ISO-10303-21;
HEADER;
FILE_DESCRIPTION (('STEP AP214'),
    '1' );
FILE_NAME ('Sheet Metal Base.step',
    '2026-10-28T16:39:03',
    ( '' ),
    ( '' ),
    'SwSTEP 2.0',
    'SolidWorks 2024',
    '' );
FILE_SCHEMA (( 'AUTOMOTIVE_DESIGN' ));
ENDSEC;

DATA;
#2=VERTEX_POINT ( 'NONE', #3957 ) ;
#5=LINE ( 'NONE', #7463, #3697 ) ;
#15=CARTESIAN_POINT ( 'NONE',  ( 199.9999999999998863, 262.5000000000000568, 0.000000000000000000 ) ) ;
#18=ORIENTED_EDGE ( 'NONE', *, *, #3876, .T. ) ;
#20=DIRECTION ( 'NONE',  ( 1.000000000000000000, 0.000000000000000000, 0.000000000000000000 ) ) ;
#22=EDGE_LOOP ( 'NONE', ( #4827, #5476, #5226, #672 ) ) ;
#26=ADVANCED_FACE ( 'NONE', ( #6325 ), #4629, .T. ) ;
#30=VERTEX_POINT ( 'NONE', #1471 ) ;
#34=ORIENTED_EDGE ( 'NONE', *, *, #3876, .F. ) ;
#35=EDGE_LOOP ( 'NONE', ( #6541, #2279, #2364, #4470, #5618 ) ) ;
#44=VECTOR ( 'NONE', #6723, 1000.000000000000000 ) ;
#45=AXIS2_PLACEMENT_3D ( 'NONE', #6354, #218, #7634 ) ;
#51=AXIS2_PLACEMENT_3D ( 'NONE', #3862, #3896, #3257 ) ;
#53=ORIENTED_EDGE ( 'NONE', *, *, #7404, .F. ) ;
#55=CIRCLE ( 'NONE', #4287, 65.50000000000000000 ) ;
#58=DIRECTION ( 'NONE',  ( 1.000000000000000000, 0.000000000000000000, 0.000000000000000000 ) ) ;
#61=ADVANCED_FACE ( 'NONE', ( #3280, #3358 ), #6366, .T. ) ;
#62=AXIS2_PLACEMENT_3D ( 'NONE', #1310, #5647, #5485 ) ;
#67=ORIENTED_EDGE ( 'NONE', *, *, #5175, .F. ) ;
#69=CARTESIAN_POINT ( 'NONE',  ( 0.000000000000000000, 0.000000000000000000, 0.000000000000000000 ) ) ;
#72=EDGE_CURVE ( 'NONE', #4343, #3684, #1276, .T. ) ;
#73=ORIENTED_EDGE ( 'NONE', *, *, #3667, .F. ) ;
#74=ORIENTED_EDGE ( 'NONE', *, *, #3629, .F. ) ;
#75=B_SPLINE_CURVE_WITH_KNOTS ( 'NONE', 3,
 ( #2455, #1205, #4890, #7349 ),
 .UNSPECIFIED., .F., .F.,
 ( 4, 4 ),
 ( 0.000000000000000000, 0.001270006434950045771 ),
 .UNSPECIFIED. ) ;
#76=EDGE_CURVE ( 'NONE', #6360, #3593, #5967, .T. ) ;
#77=ORIENTED_EDGE ( 'NONE', *, *, #5334, .F. ) ;
#79=ADVANCED_FACE ( 'NONE', ( #5146 ), #2881, .F. ) ;
#81=CARTESIAN_POINT ( 'NONE',  ( 279.9038105676658006, 161.6025403784438765, 0.000000000000000000 ) ) ;
#89=DIRECTION ( 'NONE',  ( -0.000000000000000000, -0.000000000000000000, -1.000000000000000000 ) ) ;
#91=CYLINDRICAL_SURFACE ( 'NONE', #5688, 5.000000000000004441 ) ;
#95=ORIENTED_EDGE ( 'NONE', *, *, #1155, .F. ) ;
#99=CIRCLE ( 'NONE', #3701, 12.50000000000001066 ) ;
#100=PLANE ( 'NONE',  #441 ) ;
#101=EDGE_CURVE ( 'NONE', #792, #1942, #1186, .T. ) ;
#104=CARTESIAN_POINT ( 'NONE',  ( 0.000000000000000000, 187.5000000000000000, 0.000000000000000000 ) ) ;
#113=DIRECTION ( 'NONE',  ( 0.000000000000000000, 0.000000000000000000, 1.000000000000000000 ) ) ;
#115=LINE ( 'NONE', #7340, #7495 ) ;
#117=VECTOR ( 'NONE', #1190, 1000.000000000000000 ) ;
#124=DIRECTION ( 'NONE',  ( -1.000000000000000000, 0.000000000000000000, 0.000000000000000000 ) ) ;
#129=CARTESIAN_POINT ( 'NONE',  ( 42.50000000000000000, 42.50000000000003553, 12.50000000000000000 ) ) ;
#131=LINE ( 'NONE', #1259, #5311 ) ;
#140=DIRECTION ( 'NONE',  ( -0.000000000000000000, -0.000000000000000000, -1.000000000000000000 ) ) ;
#142=CARTESIAN_POINT ( 'NONE',  ( -31.24999999999997158, 111.9999999999999289, 130.0000000000000000 ) ) ;
#143=ORIENTED_EDGE ( 'NONE', *, *, #3611, .T. ) ;
#144=VECTOR ( 'NONE', #7565, 1000.000000000000000 ) ;
#156=DIRECTION ( 'NONE',  ( 1.000000000000000000, 0.000000000000000000, 0.000000000000000000 ) ) ;
#161=VERTEX_POINT ( 'NONE', #6006 ) ;
#164=CARTESIAN_POINT ( 'NONE',  ( 42.50000000000000711, 182.5000000000000000, 12.50000000000000000 ) ) ;
#166=AXIS2_PLACEMENT_3D ( 'NONE', #651, #3778, #1809 ) ;
#168=EDGE_CURVE ( 'NONE', #511, #1117, #6645, .T. ) ;
#169=ADVANCED_FACE ( 'NONE', ( #7879 ), #5968, .T. ) ;
#170=ORIENTED_EDGE ( 'NONE', *, *, #6739, .T. ) ;
#175=CARTESIAN_POINT ( 'NONE',  ( 37.50000000000000711, 182.5000000000000000, 12.50000000000000000 ) ) ;
#177=CARTESIAN_POINT ( 'NONE',  ( 62.50000000000007105, 79.24999999999987210, 130.0000000000000000 ) ) ;
#178=ORIENTED_EDGE ( 'NONE', *, *, #7323, .T. ) ;
#183=LINE ( 'NONE', #5111, #144 ) ;
#186=DIRECTION ( 'NONE',  ( 0.5000000000000001110, 0.8660254037844385966, 0.000000000000000000 ) ) ;
#187=ORIENTED_EDGE ( 'NONE', *, *, #4482, .T. ) ;
#192=CIRCLE ( 'NONE', #5707, 5.000000000000000000 ) ;
#193=EDGE_LOOP ( 'NONE', ( #6040, #1662, #7334, #6925 ) ) ;
#195=EDGE_LOOP ( 'NONE', ( #3741, #7499, #1010, #3595 ) ) ;
#198=CARTESIAN_POINT ( 'NONE',  ( -1.301042606982605321E-15, -37.50000000000000000, 12.50000000000000000 ) ) ;
#204=CIRCLE ( 'NONE', #6347, 5.000000000000004441 ) ;
#207=DIRECTION ( 'NONE',  ( 0.000000000000000000, -0.000000000000000000, -1.000000000000000000 ) ) ;
#218=DIRECTION ( 'NONE',  ( 1.387778780781445676E-15, 1.000000000000000000, -0.000000000000000000 ) ) ;
#219=ADVANCED_FACE ( 'NONE', ( #7176 ), #3001, .F. ) ;
#220=DIRECTION ( 'NONE',  ( -1.000000000000000000, 0.000000000000000000, 0.000000000000000000 ) ) ;
#224=ORIENTED_EDGE ( 'NONE', *, *, #1037, .F. ) ;
#226=AXIS2_PLACEMENT_3D ( 'NONE', #4931, #4325, #6784 ) ;
#229=CARTESIAN_POINT ( 'NONE',  ( 286.6025403784439050, 75.00000000000002842, 12.50000000000000000 ) ) ;
#230=EDGE_LOOP ( 'NONE', ( #5895, #6013 ) ) ;
#232=CARTESIAN_POINT ( 'NONE',  ( 296.6025403784437913, 82.50000000000004263, 155.0000000000000000 ) ) ;
#233=CARTESIAN_POINT ( 'NONE',  ( -0.000000000000000000, 262.5000000000000568, 0.000000000000000000 ) ) ;
#234=CIRCLE ( 'NONE', #5486, 5.000000000000000888 ) ;
#237=EDGE_CURVE ( 'NONE', #1544, #2876, #4653, .T. ) ;
#238=EDGE_LOOP ( 'NONE', ( #6646, #5724, #7322, #559, #4232 ) ) ;
#240=ORIENTED_EDGE ( 'NONE', *, *, #6695, .T. ) ;
#242=AXIS2_PLACEMENT_3D ( 'NONE', #2614, #7029, #6306 ) ;
#253=DIRECTION ( 'NONE',  ( 1.000000000000000000, -0.000000000000000000, -0.000000000000000000 ) ) ;
#254=DIRECTION ( 'NONE',  ( -0.000000000000000000, -0.000000000000000000, -1.000000000000000000 ) ) ;
#257=ORIENTED_EDGE ( 'NONE', *, *, #7059, .T. ) ;
#262=CARTESIAN_POINT ( 'NONE',  ( -32.49999999999997158, 1.387778780781446307E-14, 0.000000000000000000 ) ) ;
#263=CARTESIAN_POINT ( 'NONE',  ( 412.5000000000000568, 82.50000000000004263, 20.00000000000000000 ) ) ;
#264=CARTESIAN_POINT ( 'NONE',  ( -37.49999999999993605, 79.24999999999992895, 130.0000000000000000 ) ) ;
#266=ORIENTED_EDGE ( 'NONE', *, *, #7571, .T. ) ;
#269=FACE_OUTER_BOUND ( 'NONE', #2507, .T. ) ;
#278=LINE ( 'NONE', #2723, #2423 ) ;
#279=VERTEX_POINT ( 'NONE', #3196 ) ;
#283=CARTESIAN_POINT ( 'NONE',  ( 314.1025403784437913, 142.5000000000000000, 125.0000000000000000 ) ) ;
#285=ORIENTED_EDGE ( 'NONE', *, *, #1155, .T. ) ;
#287=DIRECTION ( 'NONE',  ( 1.261617073437677999E-16, -1.000000000000000000, 0.000000000000000000 ) ) ;
#289=DIRECTION ( 'NONE',  ( 0.000000000000000000, 0.000000000000000000, -1.000000000000000000 ) ) ;
#294=CARTESIAN_POINT ( 'NONE',  ( 37.50000000000000711, 182.5000000000000000, 12.50000000000000000 ) ) ;
#298=ORIENTED_EDGE ( 'NONE', *, *, #6249, .T. ) ;
#301=DIRECTION ( 'NONE',  ( -0.000000000000000000, -0.000000000000000000, -1.000000000000000000 ) ) ;
#302=CARTESIAN_POINT ( 'NONE',  ( 42.50000000000000000, 47.50000000000003553, 12.65877081724072362 ) ) ;
#309=DIRECTION ( 'NONE',  ( -0.000000000000000000, 0.000000000000000000, 1.000000000000000000 ) ) ;
#311=EDGE_CURVE ( 'NONE', #1117, #1102, #5025, .T. ) ;
#315=CARTESIAN_POINT ( 'NONE',  ( 339.1025403784438481, 150.0000000000000568, 125.0000000000000000 ) ) ;
#316=AXIS2_PLACEMENT_3D ( 'NONE', #6610, #992, #3446 ) ;
#317=ADVANCED_FACE ( 'NONE', ( #7480 ), #100, .T. ) ;
#318=AXIS2_PLACEMENT_3D ( 'NONE', #1100, #546, #3630 ) ;
#319=AXIS2_PLACEMENT_3D ( 'NONE', #4648, #1727, #4057 ) ;
#324=CARTESIAN_POINT ( 'NONE',  ( 0.000000000000000000, 47.50000000000003553, 12.50000000000000000 ) ) ;
#325=LINE ( 'NONE', #7664, #747 ) ;
#331=FACE_OUTER_BOUND ( 'NONE', #5233, .T. ) ;
#336=DIRECTION ( 'NONE',  ( 4.270088556250607616E-16, 1.000000000000000000, -0.000000000000000000 ) ) ;
#337=CARTESIAN_POINT ( 'NONE',  ( -37.50000000000000000, 4.857225732735047243E-14, 12.50000000000000000 ) ) ;
#338=DIRECTION ( 'NONE',  ( 1.000000000000000000, 0.000000000000000000, 0.000000000000000000 ) ) ;
#340=MECHANICAL_DESIGN_GEOMETRIC_PRESENTATION_REPRESENTATION('',(#3420),#6113);
#343=ORIENTED_EDGE ( 'NONE', *, *, #7059, .F. ) ;
#347=CARTESIAN_POINT ( 'NONE',  ( 47.50000000000000711, 0.000000000000000000, 5.000000000000000000 ) ) ;
#350=FACE_OUTER_BOUND ( 'NONE', #6015, .T. ) ;
#353=ORIENTED_EDGE ( 'NONE', *, *, #4920, .T. ) ;
#354=CYLINDRICAL_SURFACE ( 'NONE', #5629, 37.50000000000000711 ) ;
#356=CYLINDRICAL_SURFACE ( 'NONE', #4418, 29.99999999999997158 ) ;
#358=CARTESIAN_POINT ( 'NONE',  ( -37.49999999999989342, 187.4999999999999432, 0.000000000000000000 ) ) ;
#361=CARTESIAN_POINT ( 'NONE',  ( 200.0000000000000000, 0.000000000000000000, 0.000000000000000000 ) ) ;
#362=CIRCLE ( 'NONE', #1515, 5.000000000000004441 ) ;
#363=CARTESIAN_POINT ( 'NONE',  ( 296.6025403784439050, 149.9999999999999716, 125.0000000000000000 ) ) ;
#367=EDGE_LOOP ( 'NONE', ( #1357, #4396, #4864, #3521 ) ) ;
#370=CYLINDRICAL_SURFACE ( 'NONE', #7353, 4.999999999999997335 ) ;
#371=AXIS2_PLACEMENT_3D ( 'NONE', #6748, #1998, #156 ) ;
#372=AXIS2_PLACEMENT_3D ( 'NONE', #5985, #498, #7152 ) ;
#374=EDGE_CURVE ( 'NONE', #3850, #1583, #817, .T. ) ;
#377=VECTOR ( 'NONE', #7137, 1000.000000000000000 ) ;
#380=CARTESIAN_POINT ( 'NONE',  ( 0.000000000000000000, 47.50000000000009237, 130.0000000000000000 ) ) ;
#381=DIRECTION ( 'NONE',  ( 0.000000000000000000, -0.000000000000000000, -1.000000000000000000 ) ) ;
#384=ORIENTED_EDGE ( 'NONE', *, *, #5627, .T. ) ;
#385=EDGE_CURVE ( 'NONE', #1194, #1704, #2747, .T. ) ;
#393=VERTEX_POINT ( 'NONE', #5107 ) ;
#396=ORIENTED_EDGE ( 'NONE', *, *, #1409, .T. ) ;
#397=DIRECTION ( 'NONE',  ( -0.000000000000000000, -0.000000000000000000, -1.000000000000000000 ) ) ;
#400=DIRECTION ( 'NONE',  ( 1.000000000000000000, 0.000000000000000000, 0.000000000000000000 ) ) ;
#402=CARTESIAN_POINT ( 'NONE',  ( 200.0000000000000000, 0.000000000000000000, 12.50000000000000000 ) ) ;
#403=DIRECTION ( 'NONE',  ( 1.000000000000000000, 0.000000000000000000, 0.000000000000000000 ) ) ;
#405=DIRECTION ( 'NONE',  ( -0.000000000000000000, -0.000000000000000000, -1.000000000000000000 ) ) ;
#409=PRODUCT_DEFINITION_SHAPE ( 'NONE', 'NONE',  #7906 ) ;
#413=CARTESIAN_POINT ( 'NONE',  ( 412.5000000000000568, 75.00000000000001421, 20.00000000000000000 ) ) ;
#415=DIRECTION ( 'NONE',  ( 1.000000000000000000, -4.625929269271489858E-16, 0.000000000000000000 ) ) ;
#416=CARTESIAN_POINT ( 'NONE',  ( 12.50000000000002309, 225.0000000000000284, 12.50000000000000000 ) ) ;
#424=ORIENTED_EDGE ( 'NONE', *, *, #1837, .F. ) ;
#425=ADVANCED_FACE ( 'NONE', ( #5065 ), #1542, .T. ) ;
#427=ORIENTED_EDGE ( 'NONE', *, *, #1008, .T. ) ;
#428=CIRCLE ( 'NONE', #166, 37.50000000000003553 ) ;
#429=ADVANCED_FACE ( 'NONE', ( #5224 ), #4545, .F. ) ;
#431=ORIENTED_EDGE ( 'NONE', *, *, #1211, .F. ) ;
#433=DIRECTION ( 'NONE',  ( 1.000000000000000000, -9.251858538542979716E-16, 0.000000000000000000 ) ) ;
#438=ORIENTED_EDGE ( 'NONE', *, *, #1694, .F. ) ;
#441=AXIS2_PLACEMENT_3D ( 'NONE', #1979, #6881, #1823 ) ;
#442=LINE ( 'NONE', #3529, #7380 ) ;
#444=SHAPE_REPRESENTATION ( 'Sheet Metal Base', ( #5785 ), #6420 ) ;
#447=VECTOR ( 'NONE', #405, 1000.000000000000000 ) ;
#450=ORIENTED_EDGE ( 'NONE', *, *, #864, .F. ) ;
#455=ADVANCED_FACE ( 'NONE', ( #6999 ), #897, .F. ) ;
#456=CARTESIAN_POINT ( 'NONE',  ( -12.50000000000000000, 0.000000000000000000, 12.50000000000000000 ) ) ;
#458=DIRECTION ( 'NONE',  ( 1.000000000000000000, 0.000000000000000000, -0.000000000000000000 ) ) ;
#466=VECTOR ( 'NONE', #1352, 1000.000000000000000 ) ;
#468=PLANE ( 'NONE',  #1082 ) ;
#470=EDGE_CURVE ( 'NONE', #4246, #3773, #2141, .T. ) ;
#471=CIRCLE ( 'NONE', #4940, 12.50000000000001066 ) ;
#472=ORIENTED_EDGE ( 'NONE', *, *, #6692, .T. ) ;
#477=VERTEX_POINT ( 'NONE', #934 ) ;
#481=VERTEX_POINT ( 'NONE', #2183 ) ;
#483=EDGE_CURVE ( 'NONE', #5349, #477, #7076, .T. ) ;
#484=DIRECTION ( 'NONE',  ( 0.000000000000000000, -0.000000000000000000, -1.000000000000000000 ) ) ;
#487=ORIENTED_EDGE ( 'NONE', *, *, #4999, .T. ) ;
#488=DIRECTION ( 'NONE',  ( -0.8660254037844385966, 0.5000000000000003331, 0.000000000000000000 ) ) ;
#489=CARTESIAN_POINT ( 'NONE',  ( 2.775557561562891351E-14, 225.0000000000000284, 12.50000000000000000 ) ) ;
#491=EDGE_CURVE ( 'NONE', #4246, #1194, #7560, .T. ) ;
#494=ORIENTED_EDGE ( 'NONE', *, *, #6021, .T. ) ;
#495=AXIS2_PLACEMENT_3D ( 'NONE', #1873, #6693, #562 ) ;
#498=DIRECTION ( 'NONE',  ( 0.000000000000000000, -1.000000000000000000, 0.000000000000000000 ) ) ;
#502=AXIS2_PLACEMENT_3D ( 'NONE', #7116, #975, #2909 ) ;
#505=FACE_BOUND ( 'NONE', #3911, .T. ) ;
#507=CYLINDRICAL_SURFACE ( 'NONE', #1385, 37.50000000000000711 ) ;
#511=VERTEX_POINT ( 'NONE', #263 ) ;
#512=AXIS2_PLACEMENT_3D ( 'NONE', #3984, #4796, #7779 ) ;
#515=ORIENTED_EDGE ( 'NONE', *, *, #3809, .F. ) ;
#518=ORIENTED_EDGE ( 'NONE', *, *, #3537, .T. ) ;
#524=ORIENTED_EDGE ( 'NONE', *, *, #2580, .T. ) ;
#530=VERTEX_POINT ( 'NONE', #1780 ) ;
#531=ADVANCED_FACE ( 'NONE', ( #7203 ), #1619, .F. ) ;
#535=FACE_OUTER_BOUND ( 'NONE', #6691, .T. ) ;
#546=DIRECTION ( 'NONE',  ( -0.000000000000000000, 0.000000000000000000, 1.000000000000000000 ) ) ;
#553=CARTESIAN_POINT ( 'NONE',  ( 326.6025403784438481, 150.0000000000000568, 125.0000000000000000 ) ) ;
#556=VERTEX_POINT ( 'NONE', #5306 ) ;
#558=DIRECTION ( 'NONE',  ( -4.789677997474686366E-16, -1.000000000000000000, 0.000000000000000000 ) ) ;
#559=ORIENTED_EDGE ( 'NONE', *, *, #1062, .T. ) ;
#562=DIRECTION ( 'NONE',  ( 1.000000000000000000, 0.000000000000000000, 0.000000000000000000 ) ) ;
#563=DIRECTION ( 'NONE',  ( -0.000000000000000000, -0.000000000000000000, -1.000000000000000000 ) ) ;
#568=ORIENTED_EDGE ( 'NONE', *, *, #7584, .F. ) ;
#571=CARTESIAN_POINT ( 'NONE',  ( 296.6025403784437913, 144.9999999999999716, 0.000000000000000000 ) ) ;
#572=DIRECTION ( 'NONE',  ( 1.000000000000000000, 0.000000000000000000, 0.000000000000000000 ) ) ;
#573=DIRECTION ( 'NONE',  ( 0.000000000000000000, 0.000000000000000000, 1.000000000000000000 ) ) ;
#574=VECTOR ( 'NONE', #1209, 1000.000000000000000 ) ;
#576=DIRECTION ( 'NONE',  ( 0.000000000000000000, -1.000000000000000000, 0.000000000000000000 ) ) ;
#577=CARTESIAN_POINT ( 'NONE',  ( 286.6025403784437913, 135.0000000000000000, 12.50000000000000000 ) ) ;
#579=EDGE_CURVE ( 'NONE', #2973, #7220, #2385, .T. ) ;
#580=VECTOR ( 'NONE', #728, 1000.000000000000000 ) ;
#584=DIRECTION ( 'NONE',  ( 1.000000000000000000, 0.000000000000000000, 0.000000000000000000 ) ) ;
#591=ORIENTED_EDGE ( 'NONE', *, *, #3316, .T. ) ;
#592=FACE_OUTER_BOUND ( 'NONE', #7147, .T. ) ;
#593=DIRECTION ( 'NONE',  ( -4.789677997474686366E-16, -1.000000000000000000, -0.000000000000000000 ) ) ;
#600=VERTEX_POINT ( 'NONE', #2272 ) ;
#602=VECTOR ( 'NONE', #5887, 1000.000000000000000 ) ;
#613=VECTOR ( 'NONE', #5624, 1000.000000000000000 ) ;
#615=CARTESIAN_POINT ( 'NONE',  ( 286.6025403784437913, 135.0000000000000000, 12.50000000000000000 ) ) ;
#617=VECTOR ( 'NONE', #6785, 1000.000000000000000 ) ;
#620=LINE ( 'NONE', #6874, #4152 ) ;
#621=LINE ( 'NONE', #2464, #6448 ) ;
#624=VECTOR ( 'NONE', #6475, 1000.000000000000000 ) ;
#626=ORIENTED_EDGE ( 'NONE', *, *, #4262, .T. ) ;
#627=AXIS2_PLACEMENT_3D ( 'NONE', #1428, #3879, #6326 ) ;
#630=LINE ( 'NONE', #7288, #2124 ) ;
#631=CARTESIAN_POINT ( 'NONE',  ( 0.000000000000000000, -37.50000000000000000, 12.50000000000000000 ) ) ;
#634=DIRECTION ( 'NONE',  ( -0.000000000000000000, 0.000000000000000000, 1.000000000000000000 ) ) ;
#636=DIRECTION ( 'NONE',  ( -1.000000000000000000, 0.000000000000000000, 0.000000000000000000 ) ) ;
#637=CIRCLE ( 'NONE', #1657, 37.50000000000003553 ) ;
#640=ORIENTED_EDGE ( 'NONE', *, *, #2125, .F. ) ;
#642=VERTEX_POINT ( 'NONE', #4372 ) ;
#645=ORIENTED_EDGE ( 'NONE', *, *, #5923, .T. ) ;
#647=EDGE_LOOP ( 'NONE', ( #2566, #3992, #6282, #4635, #3699, #5556, #5162, #7459 ) ) ;
#648=FACE_OUTER_BOUND ( 'NONE', #1364, .T. ) ;
#649=LINE ( 'NONE', #3103, #1509 ) ;
#651=CARTESIAN_POINT ( 'NONE',  ( 199.9999999999998863, 225.0000000000000284, 0.000000000000000000 ) ) ;
#655=LINE ( 'NONE', #7469, #7008 ) ;
#657=DIRECTION ( 'NONE',  ( -1.295260195396012940E-15, 1.000000000000000000, 0.000000000000000000 ) ) ;
#660=ORIENTED_EDGE ( 'NONE', *, *, #491, .T. ) ;
#661=EDGE_CURVE ( 'NONE', #1300, #698, #6721, .T. ) ;
#662=ORIENTED_EDGE ( 'NONE', *, *, #6661, .F. ) ;
#668=LINE ( 'NONE', #1189, #7500 ) ;
#672=ORIENTED_EDGE ( 'NONE', *, *, #2727, .T. ) ;
#675=FACE_BOUND ( 'NONE', #4183, .T. ) ;
#679=EDGE_LOOP ( 'NONE', ( #2751, #4665, #1825, #7638, #6357 ) ) ;
#684=CARTESIAN_POINT ( 'NONE',  ( -32.49999999999990052, 177.4999999999999432, 0.000000000000000000 ) ) ;
#686=VECTOR ( 'NONE', #593, 1000.000000000000000 ) ;
#696=CIRCLE ( 'NONE', #6850, 4.999999999999997335 ) ;
#698=VERTEX_POINT ( 'NONE', #733 ) ;
#707=DIRECTION ( 'NONE',  ( 0.000000000000000000, 0.000000000000000000, -1.000000000000000000 ) ) ;
#711=ORIENTED_EDGE ( 'NONE', *, *, #3197, .F. ) ;
#715=CIRCLE ( 'NONE', #2641, 12.50000000000001066 ) ;
#722=ORIENTED_EDGE ( 'NONE', *, *, #1940, .T. ) ;
#724=EDGE_CURVE ( 'NONE', #5251, #1704, #131, .T. ) ;
#727=CARTESIAN_POINT ( 'NONE',  ( 296.6025403784437913, 135.0000000000000000, 12.50000000000000000 ) ) ;
#728=DIRECTION ( 'NONE',  ( -1.000000000000000000, 4.270088556250607616E-16, -0.000000000000000000 ) ) ;
#733=CARTESIAN_POINT ( 'NONE',  ( -12.50000000000000000, 0.000000000000000000, 0.000000000000000000 ) ) ;
#734=FACE_OUTER_BOUND ( 'NONE', #2970, .T. ) ;
#746=CYLINDRICAL_SURFACE ( 'NONE', #5836, 5.000000000000000888 ) ;
#747=VECTOR ( 'NONE', #254, 1000.000000000000000 ) ;
#751=ORIENTED_EDGE ( 'NONE', *, *, #1464, .T. ) ;
#761=ORIENTED_EDGE ( 'NONE', *, *, #2422, .T. ) ;
#764=ORIENTED_EDGE ( 'NONE', *, *, #7360, .F. ) ;
#765=EDGE_CURVE ( 'NONE', #2601, #6545, #620, .T. ) ;
#769=CARTESIAN_POINT ( 'NONE',  ( -4.731064025391297956E-15, 37.50000000000004263, 12.50000000000000000 ) ) ;
#770=CARTESIAN_POINT ( 'NONE',  ( 42.50000000000000000, 37.50000000000003553, 12.50000000000000000 ) ) ;
#778=CARTESIAN_POINT ( 'NONE',  ( -4.731064025391297956E-15, 37.50000000000004263, 12.50000000000000000 ) ) ;
#780=CARTESIAN_POINT ( 'NONE',  ( 232.4759526419164217, 243.7500000000000000, 0.000000000000000000 ) ) ;
#786=ORIENTED_EDGE ( 'NONE', *, *, #483, .F. ) ;
#788=CARTESIAN_POINT ( 'NONE',  ( 296.6025403784439050, 75.00000000000007105, 5.000000000000000000 ) ) ;
#791=CARTESIAN_POINT ( 'NONE',  ( 0.000000000000000000, 262.5000000000000568, 12.50000000000000000 ) ) ;
#792=VERTEX_POINT ( 'NONE', #4862 ) ;
#805=DIRECTION ( 'NONE',  ( -4.789677997474686366E-16, -1.000000000000000000, -0.000000000000000000 ) ) ;
#809=EDGE_CURVE ( 'NONE', #1302, #4126, #3780, .T. ) ;
#817=LINE ( 'NONE', #6477, #6078 ) ;
#821=AXIS2_PLACEMENT_3D ( 'NONE', #7617, #1562, #921 ) ;
#822=AXIS2_PLACEMENT_3D ( 'NONE', #6595, #6523, #7239 ) ;
#834=ADVANCED_FACE ( 'NONE', ( #7587 ), #6949, .T. ) ;
#836=CARTESIAN_POINT ( 'NONE',  ( 412.4999999999998863, 137.4999999999999716, 12.50000000000000000 ) ) ;
#842=CARTESIAN_POINT ( 'NONE',  ( 412.5000000000000568, 142.5000000000000000, 20.00000000000000000 ) ) ;
#843=EDGE_LOOP ( 'NONE', ( #7455, #2077, #860, #494 ) ) ;
#846=VERTEX_POINT ( 'NONE', #6914 ) ;
#857=CARTESIAN_POINT ( 'NONE',  ( 412.5000000000002274, 1.221245327087672598E-12, 12.50000000000000000 ) ) ;
#860=ORIENTED_EDGE ( 'NONE', *, *, #470, .F. ) ;
#862=EDGE_CURVE ( 'NONE', #7501, #642, #7108, .T. ) ;
#864=EDGE_CURVE ( 'NONE', #5496, #5551, #2131, .T. ) ;
#870=DIRECTION ( 'NONE',  ( 0.000000000000000000, -0.000000000000000000, 1.000000000000000000 ) ) ;
#876=ORIENTED_EDGE ( 'NONE', *, *, #101, .F. ) ;
#883=CARTESIAN_POINT ( 'NONE',  ( 52.50000000000000711, 177.5000000000000000, 130.0000000000000000 ) ) ;
#885=CIRCLE ( 'NONE', #371, 5.000000000000004441 ) ;
#889=PLANE ( 'NONE',  #4085 ) ;
#890=CARTESIAN_POINT ( 'NONE',  ( 0.000000000000000000, 113.0000000000000995, 130.0000000000000000 ) ) ;
#896=DIRECTION ( 'NONE',  ( 0.000000000000000000, -0.000000000000000000, -1.000000000000000000 ) ) ;
#897=PLANE ( 'NONE',  #6204 ) ;
#902=ORIENTED_EDGE ( 'NONE', *, *, #579, .F. ) ;
#905=VERTEX_POINT ( 'NONE', #5668 ) ;
#906=LINE ( 'NONE', #6440, #7257 ) ;
#914=ORIENTED_EDGE ( 'NONE', *, *, #3379, .T. ) ;
#916=VERTEX_POINT ( 'NONE', #5827 ) ;
#917=DIRECTION ( 'NONE',  ( -0.000000000000000000, -0.000000000000000000, -1.000000000000000000 ) ) ;
#919=LINE ( 'NONE', #7058, #1634 ) ;
#921=DIRECTION ( 'NONE',  ( 0.000000000000000000, 0.000000000000000000, 1.000000000000000000 ) ) ;
#922=EDGE_LOOP ( 'NONE', ( #2515, #3791, #1468, #5188 ) ) ;
#924=DIRECTION ( 'NONE',  ( -4.237492460401360996E-16, -1.000000000000000000, 0.000000000000000000 ) ) ;
#933=LINE ( 'NONE', #7559, #624 ) ;
#934=CARTESIAN_POINT ( 'NONE',  ( 37.50000000000000711, 182.5000000000000000, 0.000000000000000000 ) ) ;
#936=VECTOR ( 'NONE', #4414, 1000.000000000000000 ) ;
#946=EDGE_CURVE ( 'NONE', #4316, #7842, #5174, .T. ) ;
#948=DIRECTION ( 'NONE',  ( -0.000000000000000000, -0.000000000000000000, -1.000000000000000000 ) ) ;
#951=VECTOR ( 'NONE', #1982, 1000.000000000000000 ) ;
#953=AXIS2_PLACEMENT_3D ( 'NONE', #7399, #1894, #4339 ) ;
#971=DIRECTION ( 'NONE',  ( -0.000000000000000000, -0.000000000000000000, -1.000000000000000000 ) ) ;
#973=CIRCLE ( 'NONE', #5457, 5.000000000000000888 ) ;
#975=DIRECTION ( 'NONE',  ( 1.000000000000000000, 0.000000000000000000, -0.000000000000000000 ) ) ;
#978=CARTESIAN_POINT ( 'NONE',  ( 42.50000000000000000, 37.50000000000003553, 0.000000000000000000 ) ) ;
#981=DIRECTION ( 'NONE',  ( 0.000000000000000000, -0.000000000000000000, -1.000000000000000000 ) ) ;
#983=CIRCLE ( 'NONE', #6493, 5.000000000000004441 ) ;
#984=ORIENTED_EDGE ( 'NONE', *, *, #1793, .F. ) ;
#987=DIRECTION ( 'NONE',  ( 0.000000000000000000, 1.000000000000000000, 0.000000000000000000 ) ) ;
#988=AXIS2_PLACEMENT_3D ( 'NONE', #324, #5863, #1565 ) ;
#989=CARTESIAN_POINT ( 'NONE',  ( 3.831742397979759191E-14, 80.00000000000021316, 5.000000000000000000 ) ) ;
#991=DIRECTION ( 'NONE',  ( -0.000000000000000000, -0.000000000000000000, -1.000000000000000000 ) ) ;
#992=DIRECTION ( 'NONE',  ( -0.000000000000000000, 0.000000000000000000, 1.000000000000000000 ) ) ;
#994=VERTEX_POINT ( 'NONE', #7069 ) ;
#997=EDGE_CURVE ( 'NONE', #1382, #7382, #7753, .T. ) ;
#1001=AXIS2_PLACEMENT_3D ( 'NONE', #1003, #488, #2856 ) ;
#1003=CARTESIAN_POINT ( 'NONE',  ( 182.4759526419164217, -105.3525403784438907, 12.50000000000000000 ) ) ;
#1008=EDGE_CURVE ( 'NONE', #4616, #792, #6217, .T. ) ;
#1009=CIRCLE ( 'NONE', #1901, 32.75000000000000000 ) ;
#1010=ORIENTED_EDGE ( 'NONE', *, *, #4531, .T. ) ;
#1015=CARTESIAN_POINT ( 'NONE',  ( 12.50000000000002309, 225.0000000000000284, 0.000000000000000000 ) ) ;
#1017=CARTESIAN_POINT ( 'NONE',  ( 0.000000000000000000, 87.50000000000005684, 12.50000000000000000 ) ) ;
#1018=EDGE_CURVE ( 'NONE', #4785, #4458, #2374, .T. ) ;
#1019=DIRECTION ( 'NONE',  ( -0.000000000000000000, 0.000000000000000000, 1.000000000000000000 ) ) ;
#1023=DIRECTION ( 'NONE',  ( -0.000000000000000000, -0.000000000000000000, -1.000000000000000000 ) ) ;
#1026=ORIENTED_EDGE ( 'NONE', *, *, #4143, .F. ) ;
#1027=EDGE_CURVE ( 'NONE', #6360, #4316, #3580, .T. ) ;
#1030=ORIENTED_EDGE ( 'NONE', *, *, #1181, .F. ) ;
#1034=PLANE ( 'NONE',  #3570 ) ;
#1036=VERTEX_POINT ( 'NONE', #4095 ) ;
#1037=EDGE_CURVE ( 'NONE', #2505, #2977, #192, .T. ) ;
#1038=LINE ( 'NONE', #4678, #3582 ) ;
#1040=CARTESIAN_POINT ( 'NONE',  ( 41.25000000000002842, 47.34122918275932079, 12.50000000000000000 ) ) ;
#1043=FACE_OUTER_BOUND ( 'NONE', #7603, .T. ) ;
#1044=CARTESIAN_POINT ( 'NONE',  ( -37.49999999999992184, 113.0000000000000995, 130.0000000000000000 ) ) ;
#1045=EDGE_LOOP ( 'NONE', ( #431, #6652, #298, #626 ) ) ;
#1046=ORIENTED_EDGE ( 'NONE', *, *, #3653, .F. ) ;
#1059=CARTESIAN_POINT ( 'NONE',  ( 0.000000000000000000, 0.000000000000000000, 12.50000000000000000 ) ) ;
#1062=EDGE_CURVE ( 'NONE', #905, #2195, #2108, .T. ) ;
#1065=EDGE_CURVE ( 'NONE', #916, #3491, #6601, .T. ) ;
#1067=CARTESIAN_POINT ( 'NONE',  ( 326.6025403784438481, 217.5000000000000284, 125.0000000000000000 ) ) ;
#1072=EDGE_LOOP ( 'NONE', ( #4106, #5003, #4749, #4193 ) ) ;
#1076=DIRECTION ( 'NONE',  ( 0.000000000000000000, -0.000000000000000000, -1.000000000000000000 ) ) ;
#1077=ORIENTED_EDGE ( 'NONE', *, *, #1837, .T. ) ;
#1081=CIRCLE ( 'NONE', #821, 32.75000000000000000 ) ;
#1082=AXIS2_PLACEMENT_3D ( 'NONE', #1059, #5956, #2833 ) ;
#1083=VECTOR ( 'NONE', #4571, 1000.000000000000000 ) ;
#1085=ORIENTED_EDGE ( 'NONE', *, *, #1062, .F. ) ;
#1094=CARTESIAN_POINT ( 'NONE',  ( -27.49999999999994671, 47.50000000000009237, 12.65877081724073783 ) ) ;
#1100=CARTESIAN_POINT ( 'NONE',  ( 0.000000000000000000, 0.000000000000000000, 12.50000000000000000 ) ) ;
#1102=VERTEX_POINT ( 'NONE', #2947 ) ;
#1104=ORIENTED_EDGE ( 'NONE', *, *, #3636, .T. ) ;
#1107=ADVANCED_FACE ( 'NONE', ( #535 ), #2863, .T. ) ;
#1111=EDGE_CURVE ( 'NONE', #2565, #6642, #3466, .T. ) ;
#1113=AXIS2_PLACEMENT_3D ( 'NONE', #5666, #805, #3255 ) ;
#1114=PLANE ( 'NONE',  #7423 ) ;
#1117=VERTEX_POINT ( 'NONE', #413 ) ;
#1118=DIRECTION ( 'NONE',  ( -1.000000000000000000, -4.789677997474691297E-16, 0.000000000000000000 ) ) ;
#1121=ORIENTED_EDGE ( 'NONE', *, *, #1545, .T. ) ;
#1123=ADVANCED_FACE ( 'NONE', ( #5296 ), #2261, .T. ) ;
#1137=FACE_OUTER_BOUND ( 'NONE', #6004, .T. ) ;
#1140=FACE_OUTER_BOUND ( 'NONE', #195, .T. ) ;
#1143=ORIENTED_EDGE ( 'NONE', *, *, #7483, .F. ) ;
#1144=CIRCLE ( 'NONE', #2950, 5.000000000000000888 ) ;
#1145=ORIENTED_EDGE ( 'NONE', *, *, #6739, .F. ) ;
#1151=LINE ( 'NONE', #5288, #6971 ) ;
#1154=EDGE_CURVE ( 'NONE', #2477, #7188, #1886, .T. ) ;
#1155=EDGE_CURVE ( 'NONE', #7046, #161, #3746, .T. ) ;
#1156=ORIENTED_EDGE ( 'NONE', *, *, #101, .T. ) ;
#1161=VERTEX_POINT ( 'NONE', #684 ) ;
#1164=DIRECTION ( 'NONE',  ( -1.000000000000000000, 0.000000000000000000, 0.000000000000000000 ) ) ;
#1166=VERTEX_POINT ( 'NONE', #4975 ) ;
#1170=CARTESIAN_POINT ( 'NONE',  ( 199.9999999999998863, 225.0000000000000284, 12.50000000000000000 ) ) ;
#1171=DIRECTION ( 'NONE',  ( 0.000000000000000000, -0.000000000000000000, -1.000000000000000000 ) ) ;
#1173=DIRECTION ( 'NONE',  ( -1.000000000000000000, 0.000000000000000000, -0.000000000000000000 ) ) ;
#1175=DIRECTION ( 'NONE',  ( 0.000000000000000000, -1.000000000000000000, 0.000000000000000000 ) ) ;
#1177=EDGE_CURVE ( 'NONE', #6088, #1102, #1769, .T. ) ;
#1178=CARTESIAN_POINT ( 'NONE',  ( 286.6025403784437913, 0.000000000000000000, 12.50000000000000000 ) ) ;
#1181=EDGE_CURVE ( 'NONE', #6545, #477, #6444, .T. ) ;
#1183=ORIENTED_EDGE ( 'NONE', *, *, #7478, .T. ) ;
#1184=CARTESIAN_POINT ( 'NONE',  ( 314.1025403784437913, 150.0000000000000568, 125.0000000000000000 ) ) ;
#1186=LINE ( 'NONE', #2923, #5690 ) ;
#1187=DIRECTION ( 'NONE',  ( -0.000000000000000000, 0.000000000000000000, 1.000000000000000000 ) ) ;
#1189=CARTESIAN_POINT ( 'NONE',  ( -0.000000000000000000, 47.50000000000003553, 0.000000000000000000 ) ) ;
#1190=DIRECTION ( 'NONE',  ( -1.000000000000000000, 0.000000000000000000, 0.000000000000000000 ) ) ;
#1191=ORIENTED_EDGE ( 'NONE', *, *, #5185, .T. ) ;
#1194=VERTEX_POINT ( 'NONE', #7900 ) ;
#1195=FACE_BOUND ( 'NONE', #1713, .T. ) ;
#1198=ORIENTED_EDGE ( 'NONE', *, *, #7805, .F. ) ;
#1201=ADVANCED_FACE ( 'NONE', ( #4367 ), #1325, .F. ) ;
#1202=CARTESIAN_POINT ( 'NONE',  ( 338.3083524847281183, 217.5000000000000284, 168.7439889854708213 ) ) ;
#1205=CARTESIAN_POINT ( 'NONE',  ( 41.66645320948619968, 177.5512430609197452, 12.50000000000000000 ) ) ;
#1207=EDGE_CURVE ( 'NONE', #2477, #4616, #6787, .T. ) ;
#1209=DIRECTION ( 'NONE',  ( 1.000000000000000000, -1.387778780781445676E-15, 0.000000000000000000 ) ) ;
#1211=EDGE_CURVE ( 'NONE', #1820, #1547, #428, .T. ) ;
#1219=DIRECTION ( 'NONE',  ( -1.000000000000000000, 0.000000000000000000, 0.000000000000000000 ) ) ;
#1222=VECTOR ( 'NONE', #6548, 1000.000000000000000 ) ;
#1224=CIRCLE ( 'NONE', #5713, 12.49999999999999467 ) ;
#1233=CIRCLE ( 'NONE', #2263, 12.50000000000000000 ) ;
#1243=ORIENTED_EDGE ( 'NONE', *, *, #3526, .F. ) ;
#1245=ORIENTED_EDGE ( 'NONE', *, *, #6404, .F. ) ;
#1249=VECTOR ( 'NONE', #3179, 1000.000000000000000 ) ;
#1250=CARTESIAN_POINT ( 'NONE',  ( 339.1025403784438481, 150.0000000000000568, 125.0000000000000000 ) ) ;
#1252=ADVANCED_FACE ( 'NONE', ( #5586 ), #6106, .F. ) ;
#1258=CARTESIAN_POINT ( 'NONE',  ( 326.6025403784438481, 142.5000000000000000, 125.0000000000000000 ) ) ;
#1259=CARTESIAN_POINT ( 'NONE',  ( -37.49999999999965183, -4.857225732735003066E-14, 0.000000000000000000 ) ) ;
#1262=AXIS2_PLACEMENT_3D ( 'NONE', #1379, #1861, #6122 ) ;
#1266=VECTOR ( 'NONE', #4939, 1000.000000000000000 ) ;
#1276=B_SPLINE_CURVE_WITH_KNOTS ( 'NONE', 3,
 ( #7605, #4554, #7009, #5806 ),
 .UNSPECIFIED., .F., .F.,
 ( 4, 4 ),
 ( 0.000000000000000000, 0.001270006434949985923 ),
 .UNSPECIFIED. ) ;
#1282=CARTESIAN_POINT ( 'NONE',  ( 296.6025403784439050, 90.00000000000001421, 0.000000000000000000 ) ) ;
#1283=EDGE_CURVE ( 'NONE', #4754, #2601, #75, .T. ) ;
#1286=ORIENTED_EDGE ( 'NONE', *, *, #6593, .T. ) ;
#1288=CARTESIAN_POINT ( 'NONE',  ( -27.49999999999989342, 187.4999999999999432, 0.000000000000000000 ) ) ;
#1296=DIRECTION ( 'NONE',  ( 0.000000000000000000, 0.000000000000000000, 1.000000000000000000 ) ) ;
#1300=VERTEX_POINT ( 'NONE', #6743 ) ;
#1302=VERTEX_POINT ( 'NONE', #1250 ) ;
#1305=CARTESIAN_POINT ( 'NONE',  ( 42.50000000000000000, 37.50000000000003553, 12.50000000000000000 ) ) ;
#1310=CARTESIAN_POINT ( 'NONE',  ( -37.49999999999992184, 111.9999999999999289, 130.0000000000000000 ) ) ;
#1318=ORIENTED_EDGE ( 'NONE', *, *, #491, .F. ) ;
#1322=EDGE_CURVE ( 'NONE', #7589, #2527, #2739, .T. ) ;
#1324=CARTESIAN_POINT ( 'NONE',  ( 42.50000000000000000, 47.50000000000003553, 12.65877081724072362 ) ) ;
#1325=CYLINDRICAL_SURFACE ( 'NONE', #4517, 74.99999999999995737 ) ;
#1326=CARTESIAN_POINT ( 'NONE',  ( 296.6025403784437913, 135.0000000000000000, 12.50000000000000000 ) ) ;
#1327=VECTOR ( 'NONE', #1568, 1000.000000000000000 ) ;
#1332=DIRECTION ( 'NONE',  ( -0.000000000000000000, 0.000000000000000000, 1.000000000000000000 ) ) ;
#1337=EDGE_LOOP ( 'NONE', ( #1191, #7737, #5657, #5850, #2431, #2191, #3607 ) ) ;
#1345=CARTESIAN_POINT ( 'NONE',  ( 0.000000000000000000, 0.000000000000000000, 12.50000000000000000 ) ) ;
#1346=EDGE_CURVE ( 'NONE', #5638, #2838, #3248, .T. ) ;
#1347=VECTOR ( 'NONE', #1173, 1000.000000000000000 ) ;
#1352=DIRECTION ( 'NONE',  ( -1.000000000000000000, 4.270088556250607616E-16, -0.000000000000000000 ) ) ;
#1355=VECTOR ( 'NONE', #917, 1000.000000000000000 ) ;
#1357=ORIENTED_EDGE ( 'NONE', *, *, #6320, .F. ) ;
#1360=EDGE_LOOP ( 'NONE', ( #4025, #2570, #7727, #6406, #2402, #2235, #3213, #914, #6734, #1030 ) ) ;
#1364=EDGE_LOOP ( 'NONE', ( #1805, #6622, #438, #7201, #5845 ) ) ;
#1366=CIRCLE ( 'NONE', #3932, 12.50000000000001066 ) ;
#1367=EDGE_CURVE ( 'NONE', #6805, #2766, #3369, .T. ) ;
#1370=DIRECTION ( 'NONE',  ( 0.000000000000000000, -1.000000000000000000, 0.000000000000000000 ) ) ;
#1373=CIRCLE ( 'NONE', #6763, 5.000000000000004441 ) ;
#1375=ORIENTED_EDGE ( 'NONE', *, *, #3903, .F. ) ;
#1379=CARTESIAN_POINT ( 'NONE',  ( 62.50000000000008527, 111.9999999999998863, 130.0000000000000000 ) ) ;
#1382=VERTEX_POINT ( 'NONE', #7021 ) ;
#1385=AXIS2_PLACEMENT_3D ( 'NONE', #2830, #5264, #5389 ) ;
#1392=CYLINDRICAL_SURFACE ( 'NONE', #2147, 32.75000000000001421 ) ;
#1394=CARTESIAN_POINT ( 'NONE',  ( 200.0000000000000000, -37.50000000000000711, 12.50000000000000000 ) ) ;
#1397=AXIS2_PLACEMENT_3D ( 'NONE', #5187, #2105, #6927 ) ;
#1399=VERTEX_POINT ( 'NONE', #2770 ) ;
#1400=EDGE_CURVE ( 'NONE', #530, #3850, #5781, .T. ) ;
#1402=DIRECTION ( 'NONE',  ( -0.4463453945640545317, -2.137850715617611764E-16, 0.8948607650084221543 ) ) ;
#1409=EDGE_CURVE ( 'NONE', #4343, #994, #1151, .T. ) ;
#1413=DIRECTION ( 'NONE',  ( -1.000000000000000000, 0.000000000000000000, 0.000000000000000000 ) ) ;
#1420=EDGE_CURVE ( 'NONE', #3234, #1820, #7369, .T. ) ;
#1427=ORIENTED_EDGE ( 'NONE', *, *, #3585, .F. ) ;
#1428=CARTESIAN_POINT ( 'NONE',  ( 52.50000000000000711, 0.000000000000000000, 12.50000000000000000 ) ) ;
#1429=DIRECTION ( 'NONE',  ( 1.000000000000000000, 0.000000000000000000, 0.000000000000000000 ) ) ;
#1439=LINE ( 'NONE', #5290, #447 ) ;
#1446=AXIS2_PLACEMENT_3D ( 'NONE', #2679, #5114, #7568 ) ;
#1449=EDGE_CURVE ( 'NONE', #3005, #5496, #696, .T. ) ;
#1451=CIRCLE ( 'NONE', #6077, 5.000000000000004441 ) ;
#1464=EDGE_CURVE ( 'NONE', #4603, #2527, #3042, .T. ) ;
#1466=DIRECTION ( 'NONE',  ( -1.000000000000000000, 0.000000000000000000, 0.000000000000000000 ) ) ;
#1468=ORIENTED_EDGE ( 'NONE', *, *, #6355, .T. ) ;
#1471=CARTESIAN_POINT ( 'NONE',  ( 286.6025403784437913, 150.0000000000000284, 12.50000000000000000 ) ) ;
#1473=DIRECTION ( 'NONE',  ( -1.000000000000000000, 3.469446951953614189E-17, 0.000000000000000000 ) ) ;
#1477=VERTEX_POINT ( 'NONE', #2436 ) ;
#1479=ORIENTED_EDGE ( 'NONE', *, *, #997, .T. ) ;
#1487=DIRECTION ( 'NONE',  ( 1.000000000000000000, 1.261617073437677999E-16, 0.000000000000000000 ) ) ;
#1490=DIRECTION ( 'NONE',  ( -1.000000000000000000, 0.000000000000000000, 0.000000000000000000 ) ) ;
#1491=EDGE_CURVE ( 'NONE', #6485, #7566, #4024, .T. ) ;
#1497=VERTEX_POINT ( 'NONE', #6125 ) ;
#1501=EDGE_CURVE ( 'NONE', #1166, #1399, #2753, .T. ) ;
#1506=UNCERTAINTY_MEASURE_WITH_UNIT (LENGTH_MEASURE( 1.000000000000000082E-05 ), #4897, 'distance_accuracy_value', 'NONE');
#1509=VECTOR ( 'NONE', #6262, 1000.000000000000000 ) ;
#1510=DIRECTION ( 'NONE',  ( -0.000000000000000000, -1.000000000000000000, -0.000000000000000000 ) ) ;
#1511=ORIENTED_EDGE ( 'NONE', *, *, #1400, .F. ) ;
#1514=CARTESIAN_POINT ( 'NONE',  ( -26.24999999999997158, 47.34122918275937053, 12.50000000000000000 ) ) ;
#1515=AXIS2_PLACEMENT_3D ( 'NONE', #3832, #6278, #20 ) ;
#1520=AXIS2_PLACEMENT_3D ( 'NONE', #3586, #3710, #1775 ) ;
#1522=AXIS2_PLACEMENT_3D ( 'NONE', #164, #207, #2050 ) ;
#1531=ORIENTED_EDGE ( 'NONE', *, *, #385, .F. ) ;
#1536=DIRECTION ( 'NONE',  ( -0.000000000000000000, -1.000000000000000000, -0.000000000000000000 ) ) ;
#1541=CARTESIAN_POINT ( 'NONE',  ( -37.50000000000000000, 4.857225732735047243E-14, 12.50000000000000000 ) ) ;
#1542=PLANE ( 'NONE',  #45 ) ;
#1544=VERTEX_POINT ( 'NONE', #264 ) ;
#1545=EDGE_CURVE ( 'NONE', #3479, #7501, #3761, .T. ) ;
#1547=VERTEX_POINT ( 'NONE', #780 ) ;
#1549=DIRECTION ( 'NONE',  ( 1.000000000000000000, -4.789677997474686366E-16, 0.000000000000000000 ) ) ;
#1551=DIRECTION ( 'NONE',  ( 0.000000000000000000, -0.000000000000000000, -1.000000000000000000 ) ) ;
#1552=DIRECTION ( 'NONE',  ( -0.000000000000000000, -0.000000000000000000, -1.000000000000000000 ) ) ;
#1557=DIRECTION ( 'NONE',  ( 1.000000000000000000, 0.000000000000000000, 0.000000000000000000 ) ) ;
#1559=DIRECTION ( 'NONE',  ( -0.000000000000000000, -0.000000000000000000, -1.000000000000000000 ) ) ;
#1562=DIRECTION ( 'NONE',  ( -1.000000000000000000, 0.000000000000000000, 0.000000000000000000 ) ) ;
#1565=DIRECTION ( 'NONE',  ( 0.000000000000000000, -0.000000000000000000, 1.000000000000000000 ) ) ;
#1567=DIRECTION ( 'NONE',  ( 1.000000000000000000, -0.000000000000000000, -0.000000000000000000 ) ) ;
#1568=DIRECTION ( 'NONE',  ( -1.000000000000000000, 4.270088556250607616E-16, -0.000000000000000000 ) ) ;
#1570=DIRECTION ( 'NONE',  ( -1.000000000000000000, 0.000000000000000000, 0.000000000000000000 ) ) ;
#1576=ORIENTED_EDGE ( 'NONE', *, *, #4704, .F. ) ;
#1582=DIRECTION ( 'NONE',  ( 1.000000000000000000, -4.270088556250607616E-16, 0.000000000000000000 ) ) ;
#1583=VERTEX_POINT ( 'NONE', #6356 ) ;
#1595=CARTESIAN_POINT ( 'NONE',  ( 326.6025403784438481, 217.5000000000000284, 125.0000000000000000 ) ) ;
#1596=ORIENTED_EDGE ( 'NONE', *, *, #1018, .F. ) ;
#1602=AXIS2_PLACEMENT_3D ( 'NONE', #2780, #7665, #2174 ) ;
#1607=DIRECTION ( 'NONE',  ( -1.000000000000000000, 0.000000000000000000, 0.000000000000000000 ) ) ;
#1610=CIRCLE ( 'NONE', #6227, 65.50000000000000000 ) ;
#1611=DIRECTION ( 'NONE',  ( -0.000000000000000000, -0.000000000000000000, -1.000000000000000000 ) ) ;
#1618=LINE ( 'NONE', #1178, #2300 ) ;
#1619=PLANE ( 'NONE',  #822 ) ;
#1621=PRODUCT ( 'Sheet Metal Base', 'Sheet Metal Base', '', ( #6672 ) ) ;
#1623=VECTOR ( 'NONE', #7760, 1000.000000000000000 ) ;
#1624=ORIENTED_EDGE ( 'NONE', *, *, #3027, .T. ) ;
#1625=ORIENTED_EDGE ( 'NONE', *, *, #3090, .T. ) ;
#1632=CARTESIAN_POINT ( 'NONE',  ( 42.50000000000000711, 182.5000000000000000, 12.50000000000000000 ) ) ;
#1634=VECTOR ( 'NONE', #1559, 1000.000000000000000 ) ;
#1636=DIRECTION ( 'NONE',  ( -0.4463453945640545317, 0.000000000000000000, 0.8948607650084221543 ) ) ;
#1642=DIRECTION ( 'NONE',  ( 1.000000000000000000, 0.000000000000000000, 0.000000000000000000 ) ) ;
#1644=EDGE_CURVE ( 'NONE', #1399, #1166, #4532, .T. ) ;
#1649=EDGE_CURVE ( 'NONE', #6259, #1787, #5027, .T. ) ;
#1653=CARTESIAN_POINT ( 'NONE',  ( 0.000000000000000000, 187.5000000000000000, 12.50000000000000000 ) ) ;
#1656=AXIS2_PLACEMENT_3D ( 'NONE', #2952, #1019, #5386 ) ;
#1657=AXIS2_PLACEMENT_3D ( 'NONE', #5253, #1689, #5295 ) ;
#1659=ADVANCED_FACE ( 'NONE', ( #2916, #5307, #3388, #5183, #7043, #5879 ), #468, .T. ) ;
#1660=CARTESIAN_POINT ( 'NONE',  ( 296.6025403784437913, 135.0000000000000000, 0.000000000000000000 ) ) ;
#1662=ORIENTED_EDGE ( 'NONE', *, *, #1367, .F. ) ;
#1663=( NAMED_UNIT ( * ) PLANE_ANGLE_UNIT ( ) SI_UNIT ( $, .RADIAN. ) );
#1666=CARTESIAN_POINT ( 'NONE',  ( -37.49999999999994316, 225.0000000000000284, 0.000000000000000000 ) ) ;
#1671=ADVANCED_FACE ( 'NONE', ( #7000 ), #5839, .F. ) ;
#1674=ORIENTED_EDGE ( 'NONE', *, *, #483, .T. ) ;
#1681=EDGE_LOOP ( 'NONE', ( #6131, #1576, #6775, #2352 ) ) ;
#1685=ORIENTED_EDGE ( 'NONE', *, *, #6692, .F. ) ;
#1689=DIRECTION ( 'NONE',  ( 0.000000000000000000, -0.000000000000000000, -1.000000000000000000 ) ) ;
#1690=DIRECTION ( 'NONE',  ( 0.000000000000000000, 1.000000000000000000, 0.000000000000000000 ) ) ;
#1693=EDGE_CURVE ( 'NONE', #1194, #4540, #6589, .T. ) ;
#1694=EDGE_CURVE ( 'NONE', #2973, #6773, #7749, .T. ) ;
#1697=ORIENTED_EDGE ( 'NONE', *, *, #1694, .T. ) ;
#1698=( NAMED_UNIT ( * ) SI_UNIT ( $, .STERADIAN. ) SOLID_ANGLE_UNIT ( ) );
#1704=VERTEX_POINT ( 'NONE', #1666 ) ;
#1705=DIRECTION ( 'NONE',  ( 1.000000000000000000, -0.000000000000000000, 0.000000000000000000 ) ) ;
#1706=ORIENTED_EDGE ( 'NONE', *, *, #2435, .F. ) ;
#1710=ORIENTED_EDGE ( 'NONE', *, *, #809, .F. ) ;
#1711=CIRCLE ( 'NONE', #6458, 65.50000000000000000 ) ;
#1712=DIRECTION ( 'NONE',  ( -0.000000000000000000, -1.000000000000000000, -0.000000000000000000 ) ) ;
#1713=EDGE_LOOP ( 'NONE', ( #7465, #7482 ) ) ;
#1716=ORIENTED_EDGE ( 'NONE', *, *, #6422, .F. ) ;
#1722=VECTOR ( 'NONE', #5401, 1000.000000000000000 ) ;
#1723=VECTOR ( 'NONE', #6712, 1000.000000000000000 ) ;
#1727=DIRECTION ( 'NONE',  ( 1.000000000000000000, -0.000000000000000000, -0.000000000000000000 ) ) ;
#1731=CIRCLE ( 'NONE', #2632, 5.000000000000000888 ) ;
#1736=DIRECTION ( 'NONE',  ( 0.000000000000000000, 1.000000000000000000, 0.000000000000000000 ) ) ;
#1737=VECTOR ( 'NONE', #7454, 1000.000000000000000 ) ;
#1739=DIRECTION ( 'NONE',  ( -0.000000000000000000, -0.000000000000000000, -1.000000000000000000 ) ) ;
#1744=ORIENTED_EDGE ( 'NONE', *, *, #3921, .T. ) ;
#1753=CARTESIAN_POINT ( 'NONE',  ( 52.50000000000000711, 112.5000000000000142, 195.4980915752512658 ) ) ;
#1755=FACE_OUTER_BOUND ( 'NONE', #922, .T. ) ;
#1758=EDGE_LOOP ( 'NONE', ( #5121, #1183, #2583, #4790, #4354, #427, #2179, #5281 ) ) ;
#1759=LINE ( 'NONE', #2405, #6658 ) ;
#1767=CARTESIAN_POINT ( 'NONE',  ( -31.24999999999997158, 47.50000000000009237, 195.5000000000000000 ) ) ;
#1768=DIRECTION ( 'NONE',  ( 0.000000000000000000, 1.000000000000000000, -0.000000000000000000 ) ) ;
#1769=LINE ( 'NONE', #6667, #6060 ) ;
#1771=CARTESIAN_POINT ( 'NONE',  ( 52.50000000000000711, 47.50000000000003553, 5.000000000000000000 ) ) ;
#1775=DIRECTION ( 'NONE',  ( 0.000000000000000000, 0.000000000000000000, 1.000000000000000000 ) ) ;
#1777=AXIS2_PLACEMENT_3D ( 'NONE', #2379, #4219, #5466 ) ;
#1780=CARTESIAN_POINT ( 'NONE',  ( 296.6025403784439050, 75.00000000000007105, 125.0000000000000000 ) ) ;
#1782=ORIENTED_EDGE ( 'NONE', *, *, #5595, .F. ) ;
#1787=VERTEX_POINT ( 'NONE', #3717 ) ;
#1788=CARTESIAN_POINT ( 'NONE',  ( 42.50000000000000000, 42.50000000000003553, 0.000000000000000000 ) ) ;
#1790=CARTESIAN_POINT ( 'NONE',  ( 199.9999999999998863, 262.5000000000000568, 12.50000000000000000 ) ) ;
#1791=ORIENTED_EDGE ( 'NONE', *, *, #997, .F. ) ;
#1792=DIRECTION ( 'NONE',  ( 0.000000000000000000, 0.000000000000000000, 1.000000000000000000 ) ) ;
#1793=EDGE_CURVE ( 'NONE', #3990, #5178, #2428, .T. ) ;
#1794=ORIENTED_EDGE ( 'NONE', *, *, #3903, .T. ) ;
#1795=EDGE_CURVE ( 'NONE', #1942, #7523, #6090, .T. ) ;
#1797=ORIENTED_EDGE ( 'NONE', *, *, #7679, .F. ) ;
#1805=ORIENTED_EDGE ( 'NONE', *, *, #6404, .T. ) ;
#1806=DIRECTION ( 'NONE',  ( 1.000000000000000000, 0.000000000000000000, 0.000000000000000000 ) ) ;
#1808=DIRECTION ( 'NONE',  ( 0.000000000000000000, -0.000000000000000000, -1.000000000000000000 ) ) ;
#1809=DIRECTION ( 'NONE',  ( 1.000000000000000000, 1.480297366166874072E-15, 0.000000000000000000 ) ) ;
#1811=CARTESIAN_POINT ( 'NONE',  ( 326.6025403784437913, 82.50000000000004263, 125.0000000000000000 ) ) ;
#1813=ADVANCED_FACE ( 'NONE', ( #7204 ), #6675, .T. ) ;
#1819=DIRECTION ( 'NONE',  ( -1.000000000000000000, 0.000000000000000000, 0.000000000000000000 ) ) ;
#1820=VERTEX_POINT ( 'NONE', #15 ) ;
#1822=DIRECTION ( 'NONE',  ( -0.000000000000000000, -0.000000000000000000, -1.000000000000000000 ) ) ;
#1823=DIRECTION ( 'NONE',  ( 0.000000000000000000, -0.000000000000000000, 1.000000000000000000 ) ) ;
#1825=ORIENTED_EDGE ( 'NONE', *, *, #5650, .F. ) ;
#1826=CARTESIAN_POINT ( 'NONE',  ( 338.3083524847281183, 217.5000000000000284, 168.7439889854708213 ) ) ;
#1828=ORIENTED_EDGE ( 'NONE', *, *, #809, .T. ) ;
#1834=EDGE_CURVE ( 'NONE', #1477, #2101, #6075, .T. ) ;
#1837=EDGE_CURVE ( 'NONE', #6805, #4679, #7093, .T. ) ;
#1838=ADVANCED_FACE ( 'NONE', ( #7321 ), #7241, .T. ) ;
#1841=DIRECTION ( 'NONE',  ( -0.000000000000000000, -0.000000000000000000, -1.000000000000000000 ) ) ;
#1848=VECTOR ( 'NONE', #5787, 1000.000000000000000 ) ;
#1852=DIRECTION ( 'NONE',  ( 0.4463453945640545317, 0.000000000000000000, -0.8948607650084221543 ) ) ;
#1857=VECTOR ( 'NONE', #5171, 1000.000000000000000 ) ;
#1859=VERTEX_POINT ( 'NONE', #7359 ) ;
#1861=DIRECTION ( 'NONE',  ( -1.000000000000000000, 4.270088556250607616E-16, -0.000000000000000000 ) ) ;
#1872=VERTEX_POINT ( 'NONE', #4141 ) ;
#1873=CARTESIAN_POINT ( 'NONE',  ( 2.775557561562891351E-14, 225.0000000000000284, 0.000000000000000000 ) ) ;
#1874=CYLINDRICAL_SURFACE ( 'NONE', #2887, 32.75000000000001421 ) ;
#1875=AXIS2_PLACEMENT_3D ( 'NONE', #4378, #5105, #6236 ) ;
#1880=ADVANCED_FACE ( 'NONE', ( #1140 ), #6117, .F. ) ;
#1885=VECTOR ( 'NONE', #253, 1000.000000000000000 ) ;
#1886=LINE ( 'NONE', #727, #2593 ) ;
#1893=LINE ( 'NONE', #2539, #1266 ) ;
#1894=DIRECTION ( 'NONE',  ( -4.789677997474686366E-16, -1.000000000000000000, 0.000000000000000000 ) ) ;
#1896=AXIS2_PLACEMENT_3D ( 'NONE', #1904, #1822, #2624 ) ;
#1897=EDGE_CURVE ( 'NONE', #5251, #4917, #621, .T. ) ;
#1901=AXIS2_PLACEMENT_3D ( 'NONE', #2696, #5826, #924 ) ;
#1902=EDGE_LOOP ( 'NONE', ( #1828, #4886 ) ) ;
#1904=CARTESIAN_POINT ( 'NONE',  ( 291.6025403784437913, 135.0000000000000000, 12.50000000000000000 ) ) ;
#1909=AXIS2_PLACEMENT_3D ( 'NONE', #7258, #484, #4839 ) ;
#1910=VECTOR ( 'NONE', #5503, 1000.000000000000000 ) ;
#1916=PLANE ( 'NONE',  #5745 ) ;
#1917=DIRECTION ( 'NONE',  ( -4.237492460401359023E-16, -1.000000000000000000, 0.000000000000000000 ) ) ;
#1919=VERTEX_POINT ( 'NONE', #3189 ) ;
#1925=DIRECTION ( 'NONE',  ( 1.000000000000000000, 0.000000000000000000, 0.000000000000000000 ) ) ;
#1928=CIRCLE ( 'NONE', #6549, 5.000000000000004441 ) ;
#1929=DIRECTION ( 'NONE',  ( 0.000000000000000000, 1.000000000000000000, 0.000000000000000000 ) ) ;
#1930=LINE ( 'NONE', #3032, #5621 ) ;
#1938=FACE_OUTER_BOUND ( 'NONE', #5083, .T. ) ;
#1940=EDGE_CURVE ( 'NONE', #1161, #6259, #4667, .T. ) ;
#1942=VERTEX_POINT ( 'NONE', #5097 ) ;
#1943=DIRECTION ( 'NONE',  ( -0.000000000000000000, -1.000000000000000000, -0.000000000000000000 ) ) ;
#1951=ADVANCED_FACE ( 'NONE', ( #734 ), #2579, .F. ) ;
#1952=ORIENTED_EDGE ( 'NONE', *, *, #5255, .F. ) ;
#1953=ORIENTED_EDGE ( 'NONE', *, *, #3393, .T. ) ;
#1954=ORIENTED_EDGE ( 'NONE', *, *, #1793, .T. ) ;
#1957=PLANE ( 'NONE',  #4195 ) ;
#1958=EDGE_LOOP ( 'NONE', ( #1685, #4764, #5104, #1952 ) ) ;
#1969=CARTESIAN_POINT ( 'NONE',  ( 291.6025403784439050, 90.00000000000001421, 12.50000000000000000 ) ) ;
#1972=EDGE_LOOP ( 'NONE', ( #5109, #4668, #3473, #2524 ) ) ;
#1979=CARTESIAN_POINT ( 'NONE',  ( 0.000000000000000000, 177.5000000000000000, 12.50000000000000000 ) ) ;
#1981=AXIS2_PLACEMENT_3D ( 'NONE', #5791, #3467, #289 ) ;
#1982=DIRECTION ( 'NONE',  ( -4.270088556250607616E-16, -1.000000000000000000, 0.000000000000000000 ) ) ;
#1985=EDGE_CURVE ( 'NONE', #3684, #2973, #4498, .T. ) ;
#1986=ADVANCED_FACE ( 'NONE', ( #4454 ), #91, .F. ) ;
#1998=DIRECTION ( 'NONE',  ( -0.000000000000000000, 0.000000000000000000, 1.000000000000000000 ) ) ;
#1999=VERTEX_POINT ( 'NONE', #6875 ) ;
#2000=EDGE_LOOP ( 'NONE', ( #4198, #7225, #2547, #984 ) ) ;
#2008=VECTOR ( 'NONE', #2981, 1000.000000000000000 ) ;
#2010=DIRECTION ( 'NONE',  ( 1.000000000000000000, 2.960594732333750117E-15, -0.000000000000000000 ) ) ;
#2013=DIRECTION ( 'NONE',  ( -0.000000000000000000, 1.000000000000000000, -0.000000000000000000 ) ) ;
#2022=DIRECTION ( 'NONE',  ( 1.000000000000000000, 0.000000000000000000, 0.000000000000000000 ) ) ;
#2024=VERTEX_POINT ( 'NONE', #5055 ) ;
#2033=FACE_BOUND ( 'NONE', #3555, .T. ) ;
#2041=VERTEX_POINT ( 'NONE', #7112 ) ;
#2050=DIRECTION ( 'NONE',  ( 1.000000000000000000, 0.000000000000000000, 0.000000000000000000 ) ) ;
#2055=LINE ( 'NONE', #6430, #7539 ) ;
#2060=CARTESIAN_POINT ( 'NONE',  ( -37.49999999999965183, -4.857225732735003066E-14, 12.50000000000000000 ) ) ;
#2061=DIRECTION ( 'NONE',  ( -1.000000000000000000, 0.000000000000000000, 0.000000000000000000 ) ) ;
#2062=ORIENTED_EDGE ( 'NONE', *, *, #1346, .F. ) ;
#2065=VERTEX_POINT ( 'NONE', #3342 ) ;
#2070=EDGE_CURVE ( 'NONE', #1787, #161, #5445, .T. ) ;
#2072=PLANE ( 'NONE',  #3900 ) ;
#2075=ORIENTED_EDGE ( 'NONE', *, *, #3379, .F. ) ;
#2077=ORIENTED_EDGE ( 'NONE', *, *, #3083, .F. ) ;
#2078=EDGE_CURVE ( 'NONE', #1102, #530, #6470, .T. ) ;
#2081=DIRECTION ( 'NONE',  ( 0.000000000000000000, 1.000000000000000000, 0.000000000000000000 ) ) ;
#2085=EDGE_CURVE ( 'NONE', #2565, #7589, #5866, .T. ) ;
#2091=CARTESIAN_POINT ( 'NONE',  ( 296.6025403784439618, 217.5000000000000568, 125.0000000000000000 ) ) ;
#2092=ORIENTED_EDGE ( 'NONE', *, *, #1985, .T. ) ;
#2093=ADVANCED_FACE ( 'NONE', ( #3976 ), #370, .F. ) ;
#2095=CARTESIAN_POINT ( 'NONE',  ( 296.6025403784437913, 137.4999999999999716, 17.49999999999998934 ) ) ;
#2098=CARTESIAN_POINT ( 'NONE',  ( 339.1025403784437913, 82.50000000000004263, 125.0000000000000000 ) ) ;
#2099=CARTESIAN_POINT ( 'NONE',  ( 296.6025403784437913, 87.50000000000005684, 17.49999999999998934 ) ) ;
#2101=VERTEX_POINT ( 'NONE', #7666 ) ;
#2105=DIRECTION ( 'NONE',  ( 0.000000000000000000, 1.000000000000000000, 0.000000000000000000 ) ) ;
#2108=CIRCLE ( 'NONE', #319, 65.50000000000000000 ) ;
#2112=DIRECTION ( 'NONE',  ( 0.000000000000000000, 1.000000000000000000, 0.000000000000000000 ) ) ;
#2113=LINE ( 'NONE', #4038, #6469 ) ;
#2117=AXIS2_PLACEMENT_3D ( 'NONE', #5966, #3357, #4628 ) ;
#2118=ORIENTED_EDGE ( 'NONE', *, *, #2314, .F. ) ;
#2119=CARTESIAN_POINT ( 'NONE',  ( -37.49999999999965183, -4.857225732735003066E-14, 12.50000000000000000 ) ) ;
#2120=DIRECTION ( 'NONE',  ( -0.000000000000000000, -0.000000000000000000, -1.000000000000000000 ) ) ;
#2124=VECTOR ( 'NONE', #3680, 1000.000000000000000 ) ;
#2125=EDGE_CURVE ( 'NONE', #2853, #2024, #6842, .T. ) ;
#2126=VERTEX_POINT ( 'NONE', #1015 ) ;
#2129=CARTESIAN_POINT ( 'NONE',  ( 353.4483633286965301, 82.50000000000004263, 138.3903618369216417 ) ) ;
#2131=LINE ( 'NONE', #770, #1083 ) ;
#2138=EDGE_LOOP ( 'NONE', ( #3240, #7117, #424, #2597 ) ) ;
#2141=LINE ( 'NONE', #3431, #6459 ) ;
#2146=VERTEX_POINT ( 'NONE', #5828 ) ;
#2147=AXIS2_PLACEMENT_3D ( 'NONE', #2562, #3919, #3325 ) ;
#2152=CARTESIAN_POINT ( 'NONE',  ( 41.25000000000002842, 47.34122918275932079, 12.50000000000000000 ) ) ;
#2154=DIRECTION ( 'NONE',  ( 1.000000000000000000, 0.000000000000000000, 0.000000000000000000 ) ) ;
#2157=EDGE_CURVE ( 'NONE', #3721, #642, #4612, .T. ) ;
#2159=DIRECTION ( 'NONE',  ( 0.000000000000000000, 0.000000000000000000, 1.000000000000000000 ) ) ;
#2162=CARTESIAN_POINT ( 'NONE',  ( 0.000000000000000000, 0.000000000000000000, 12.50000000000000000 ) ) ;
#2170=VECTOR ( 'NONE', #1768, 1000.000000000000000 ) ;
#2174=DIRECTION ( 'NONE',  ( 1.000000000000000000, 0.000000000000000000, 0.000000000000000000 ) ) ;
#2179=ORIENTED_EDGE ( 'NONE', *, *, #3656, .F. ) ;
#2181=CARTESIAN_POINT ( 'NONE',  ( 2.775557561562891351E-14, 225.0000000000000284, 12.50000000000000000 ) ) ;
#2183=CARTESIAN_POINT ( 'NONE',  ( 46.25000000000002842, 177.5000000000000000, 130.0000000000000000 ) ) ;
#2184=APPLICATION_CONTEXT ( 'automotive_design' ) ;
#2188=ORIENTED_EDGE ( 'NONE', *, *, #4350, .T. ) ;
#2189=EDGE_CURVE ( 'NONE', #3802, #5551, #4769, .T. ) ;
#2191=ORIENTED_EDGE ( 'NONE', *, *, #3784, .F. ) ;
#2192=PLANE ( 'NONE',  #2117 ) ;
#2193=ORIENTED_EDGE ( 'NONE', *, *, #4457, .T. ) ;
#2195=VERTEX_POINT ( 'NONE', #5946 ) ;
#2196=CARTESIAN_POINT ( 'NONE',  ( 42.50000000000000711, 182.5000000000000000, 12.50000000000000000 ) ) ;
#2197=DIRECTION ( 'NONE',  ( 1.000000000000000000, -3.469446951953614189E-17, 0.000000000000000000 ) ) ;
#2200=EDGE_LOOP ( 'NONE', ( #5796, #2704, #1121, #5767 ) ) ;
#2202=ORIENTED_EDGE ( 'NONE', *, *, #3027, .F. ) ;
#2206=EDGE_CURVE ( 'NONE', #5860, #600, #6586, .T. ) ;
#2209=CARTESIAN_POINT ( 'NONE',  ( 353.4483633286965301, 142.5000000000000000, 138.3903618369216417 ) ) ;
#2210=AXIS2_PLACEMENT_3D ( 'NONE', #2983, #458, #2904 ) ;
#2212=VECTOR ( 'NONE', #3066, 1000.000000000000000 ) ;
#2213=EDGE_CURVE ( 'NONE', #600, #3816, #2417, .T. ) ;
#2224=CARTESIAN_POINT ( 'NONE',  ( -26.24999999999997158, 47.34122918275937053, 12.50000000000000000 ) ) ;
#2226=VERTEX_POINT ( 'NONE', #7231 ) ;
#2233=ADVANCED_FACE ( 'NONE', ( #4735 ), #3541, .F. ) ;
#2235=ORIENTED_EDGE ( 'NONE', *, *, #2189, .F. ) ;
#2237=VECTOR ( 'NONE', #4368, 1000.000000000000000 ) ;
#2244=AXIS2_PLACEMENT_3D ( 'NONE', #5555, #1187, #58 ) ;
#2251=CARTESIAN_POINT ( 'NONE',  ( 353.4483633286965301, 217.5000000000000284, 138.3903618369216417 ) ) ;
#2253=VECTOR ( 'NONE', #563, 1000.000000000000000 ) ;
#2255=EDGE_CURVE ( 'NONE', #4458, #5006, #1451, .T. ) ;
#2261=CYLINDRICAL_SURFACE ( 'NONE', #6821, 65.50000000000000000 ) ;
#2263=AXIS2_PLACEMENT_3D ( 'NONE', #2162, #7696, #7184 ) ;
#2269=VERTEX_POINT ( 'NONE', #4172 ) ;
#2272=CARTESIAN_POINT ( 'NONE',  ( -37.49999999999995026, 37.50000000000010658, 0.000000000000000000 ) ) ;
#2279=ORIENTED_EDGE ( 'NONE', *, *, #1409, .F. ) ;
#2282=DIRECTION ( 'NONE',  ( 1.000000000000000000, 0.000000000000000000, 0.000000000000000000 ) ) ;
#2284=CYLINDRICAL_SURFACE ( 'NONE', #3708, 5.000000000000004441 ) ;
#2286=AXIS2_PLACEMENT_3D ( 'NONE', #7698, #6499, #6644 ) ;
#2289=ORIENTED_EDGE ( 'NONE', *, *, #7584, .T. ) ;
#2292=VECTOR ( 'NONE', #4684, 1000.000000000000000 ) ;
#2293=EDGE_CURVE ( 'NONE', #1872, #5638, #5944, .T. ) ;
#2298=EDGE_LOOP ( 'NONE', ( #3498, #5134, #4168, #7916 ) ) ;
#2299=AXIS2_PLACEMENT_3D ( 'NONE', #2095, #3265, #7628 ) ;
#2300=VECTOR ( 'NONE', #3626, 1000.000000000000000 ) ;
#2304=CARTESIAN_POINT ( 'NONE',  ( 296.6025403784437913, 149.9999999999999716, 12.50000000000000000 ) ) ;
#2308=PLANE ( 'NONE',  #502 ) ;
#2314=EDGE_CURVE ( 'NONE', #3534, #7382, #2905, .T. ) ;
#2324=CARTESIAN_POINT ( 'NONE',  ( 199.9999999999998863, 225.0000000000000284, 12.50000000000000000 ) ) ;
#2325=VERTEX_POINT ( 'NONE', #6628 ) ;
#2337=DIRECTION ( 'NONE',  ( 0.000000000000000000, -1.000000000000000000, 0.000000000000000000 ) ) ;
#2341=VECTOR ( 'NONE', #7860, 1000.000000000000000 ) ;
#2342=EDGE_CURVE ( 'NONE', #3094, #481, #1711, .T. ) ;
#2348=VERTEX_POINT ( 'NONE', #5587 ) ;
#2349=EDGE_CURVE ( 'NONE', #994, #1161, #6744, .T. ) ;
#2351=DIRECTION ( 'NONE',  ( 1.000000000000000000, 0.000000000000000000, 0.000000000000000000 ) ) ;
#2352=ORIENTED_EDGE ( 'NONE', *, *, #2919, .F. ) ;
#2353=DIRECTION ( 'NONE',  ( 1.000000000000000000, 0.000000000000000000, 0.000000000000000000 ) ) ;
#2364=ORIENTED_EDGE ( 'NONE', *, *, #72, .T. ) ;
#2367=ORIENTED_EDGE ( 'NONE', *, *, #5670, .F. ) ;
#2368=EDGE_LOOP ( 'NONE', ( #1143, #6715, #3632, #3449 ) ) ;
#2374=LINE ( 'NONE', #4130, #1222 ) ;
#2377=LINE ( 'NONE', #4814, #4801 ) ;
#2378=AXIS2_PLACEMENT_3D ( 'NONE', #7670, #1536, #5909 ) ;
#2379=CARTESIAN_POINT ( 'NONE',  ( 326.6025403784438481, 150.0000000000000568, 125.0000000000000000 ) ) ;
#2382=CARTESIAN_POINT ( 'NONE',  ( 52.50000000000000711, 47.50000000000003553, 130.0000000000000000 ) ) ;
#2385=B_SPLINE_CURVE_WITH_KNOTS ( 'NONE', 3,
 ( #2224, #7837, #6674, #6635 ),
 .UNSPECIFIED., .F., .F.,
 ( 4, 4 ),
 ( 0.000000000000000000, 0.001270006434950044904 ),
 .UNSPECIFIED. ) ;
#2386=DIRECTION ( 'NONE',  ( -1.000000000000000000, -2.960594732333750117E-15, 0.000000000000000000 ) ) ;
#2396=ORIENTED_EDGE ( 'NONE', *, *, #3311, .F. ) ;
#2399=ORIENTED_EDGE ( 'NONE', *, *, #3554, .T. ) ;
#2400=CIRCLE ( 'NONE', #3551, 65.50000000000000000 ) ;
#2402=ORIENTED_EDGE ( 'NONE', *, *, #5255, .T. ) ;
#2405=CARTESIAN_POINT ( 'NONE',  ( 412.5000000000001137, 217.5000000000000000, 20.00000000000000000 ) ) ;
#2408=VECTOR ( 'NONE', #1841, 1000.000000000000000 ) ;
#2409=ORIENTED_EDGE ( 'NONE', *, *, #7191, .T. ) ;
#2417=LINE ( 'NONE', #5384, #574 ) ;
#2419=CIRCLE ( 'NONE', #1522, 5.000000000000004441 ) ;
#2422=EDGE_CURVE ( 'NONE', #1166, #1544, #3217, .T. ) ;
#2423=VECTOR ( 'NONE', #5152, 1000.000000000000000 ) ;
#2428=LINE ( 'NONE', #5996, #4030 ) ;
#2431=ORIENTED_EDGE ( 'NONE', *, *, #3311, .T. ) ;
#2435=EDGE_CURVE ( 'NONE', #5563, #6259, #6226, .T. ) ;
#2436=CARTESIAN_POINT ( 'NONE',  ( 212.4999999999999147, 225.0000000000000284, 12.50000000000000000 ) ) ;
#2438=CARTESIAN_POINT ( 'NONE',  ( 41.25000000000002842, 0.000000000000000000, 17.50000000000000000 ) ) ;
#2439=ADVANCED_FACE ( 'NONE', ( #4935 ), #5090, .T. ) ;
#2440=ORIENTED_EDGE ( 'NONE', *, *, #1008, .F. ) ;
#2442=ORIENTED_EDGE ( 'NONE', *, *, #3393, .F. ) ;
#2444=ORIENTED_EDGE ( 'NONE', *, *, #3470, .F. ) ;
#2449=AXIS2_PLACEMENT_3D ( 'NONE', #5987, #7111, #3501 ) ;
#2451=ORIENTED_EDGE ( 'NONE', *, *, #1464, .F. ) ;
#2453=DIRECTION ( 'NONE',  ( 1.000000000000000000, 0.000000000000000000, 0.000000000000000000 ) ) ;
#2455=CARTESIAN_POINT ( 'NONE',  ( 41.25000000000002842, 177.6587708172407076, 12.50000000000000000 ) ) ;
#2464=CARTESIAN_POINT ( 'NONE',  ( -0.000000000000000000, 187.4999999999999432, 0.000000000000000000 ) ) ;
#2472=DIRECTION ( 'NONE',  ( 1.000000000000000000, 0.000000000000000000, 0.000000000000000000 ) ) ;
#2477=VERTEX_POINT ( 'NONE', #1326 ) ;
#2481=FACE_OUTER_BOUND ( 'NONE', #2368, .T. ) ;
#2487=AXIS2_PLACEMENT_3D ( 'NONE', #553, #5482, #2282 ) ;
#2489=ORIENTED_EDGE ( 'NONE', *, *, #3807, .F. ) ;
#2490=CYLINDRICAL_SURFACE ( 'NONE', #226, 4.999999999999997335 ) ;
#2494=DIRECTION ( 'NONE',  ( 0.000000000000000000, 0.000000000000000000, -1.000000000000000000 ) ) ;
#2495=VECTOR ( 'NONE', #7655, 1000.000000000000000 ) ;
#2496=CARTESIAN_POINT ( 'NONE',  ( 62.50000000000007105, 79.24999999999987210, 130.0000000000000000 ) ) ;
#2497=AXIS2_PLACEMENT_3D ( 'NONE', #142, #220, #2588 ) ;
#2499=FACE_OUTER_BOUND ( 'NONE', #5406, .T. ) ;
#2500=CARTESIAN_POINT ( 'NONE',  ( -37.49999999999995026, 37.50000000000010658, 12.50000000000000000 ) ) ;
#2501=CARTESIAN_POINT ( 'NONE',  ( 0.000000000000000000, 0.000000000000000000, 0.000000000000000000 ) ) ;
#2505=VERTEX_POINT ( 'NONE', #7701 ) ;
#2507=EDGE_LOOP ( 'NONE', ( #6851, #1156, #568, #3769, #4549 ) ) ;
#2512=EDGE_LOOP ( 'NONE', ( #1625, #240, #6975, #5598, #67 ) ) ;
#2513=LINE ( 'NONE', #4954, #3790 ) ;
#2515=ORIENTED_EDGE ( 'NONE', *, *, #6411, .F. ) ;
#2519=AXIS2_PLACEMENT_3D ( 'NONE', #129, #4451, #3148 ) ;
#2521=DIRECTION ( 'NONE',  ( 1.000000000000000000, 0.000000000000000000, 0.000000000000000000 ) ) ;
#2522=FACE_OUTER_BOUND ( 'NONE', #2200, .T. ) ;
#2523=VECTOR ( 'NONE', #3819, 1000.000000000000000 ) ;
#2524=ORIENTED_EDGE ( 'NONE', *, *, #2422, .F. ) ;
#2525=ORIENTED_EDGE ( 'NONE', *, *, #4737, .T. ) ;
#2527=VERTEX_POINT ( 'NONE', #2209 ) ;
#2528=CARTESIAN_POINT ( 'NONE',  ( 412.4999999999998295, 150.0000000000000284, 5.000000000000000000 ) ) ;
#2533=EDGE_CURVE ( 'NONE', #2900, #6485, #1439, .T. ) ;
#2537=SHAPE_DEFINITION_REPRESENTATION ( #409, #444 ) ;
#2539=CARTESIAN_POINT ( 'NONE',  ( 5.204170427930428856E-14, 37.50000000000005684, 12.50000000000000000 ) ) ;
#2547=ORIENTED_EDGE ( 'NONE', *, *, #4245, .F. ) ;
#2553=CARTESIAN_POINT ( 'NONE',  ( 41.25000000000002842, 177.5000000000000000, 17.50000000000000000 ) ) ;
#2557=ORIENTED_EDGE ( 'NONE', *, *, #3197, .T. ) ;
#2561=ORIENTED_EDGE ( 'NONE', *, *, #4980, .F. ) ;
#2562=CARTESIAN_POINT ( 'NONE',  ( 62.50000000000008527, 111.9999999999998863, 130.0000000000000000 ) ) ;
#2565=VERTEX_POINT ( 'NONE', #363 ) ;
#2566=ORIENTED_EDGE ( 'NONE', *, *, #4482, .F. ) ;
#2569=CARTESIAN_POINT ( 'NONE',  ( 286.6025403784439050, 0.000000000000000000, 0.000000000000000000 ) ) ;
#2570=ORIENTED_EDGE ( 'NONE', *, *, #7730, .T. ) ;
#2579=CYLINDRICAL_SURFACE ( 'NONE', #5051, 12.50000000000000000 ) ;
#2580=EDGE_CURVE ( 'NONE', #3479, #3721, #1081, .T. ) ;
#2583=ORIENTED_EDGE ( 'NONE', *, *, #7191, .F. ) ;
#2588=DIRECTION ( 'NONE',  ( 0.000000000000000000, 0.000000000000000000, 1.000000000000000000 ) ) ;
#2593=VECTOR ( 'NONE', #4215, 1000.000000000000000 ) ;
#2595=ORIENTED_EDGE ( 'NONE', *, *, #4875, .F. ) ;
#2597=ORIENTED_EDGE ( 'NONE', *, *, #1367, .T. ) ;
#2599=CARTESIAN_POINT ( 'NONE',  ( -37.49999999999990763, 144.7499999999999432, 130.0000000000000000 ) ) ;
#2601=VERTEX_POINT ( 'NONE', #6419 ) ;
#2602=CARTESIAN_POINT ( 'NONE',  ( 286.6025403784437913, 135.0000000000000000, 0.000000000000000000 ) ) ;
#2603=ORIENTED_EDGE ( 'NONE', *, *, #7440, .T. ) ;
#2604=ORIENTED_EDGE ( 'NONE', *, *, #5227, .T. ) ;
#2609=AXIS2_PLACEMENT_3D ( 'NONE', #3863, #2013, #3789 ) ;
#2614=CARTESIAN_POINT ( 'NONE',  ( 42.50000000000000000, 42.50000000000003553, 12.50000000000000000 ) ) ;
#2621=FACE_OUTER_BOUND ( 'NONE', #3613, .T. ) ;
#2622=ORIENTED_EDGE ( 'NONE', *, *, #4401, .F. ) ;
#2624=DIRECTION ( 'NONE',  ( -1.000000000000000000, 0.000000000000000000, 0.000000000000000000 ) ) ;
#2625=VECTOR ( 'NONE', #7381, 1000.000000000000000 ) ;
#2627=AXIS2_PLACEMENT_3D ( 'NONE', #4572, #5211, #415 ) ;
#2632=AXIS2_PLACEMENT_3D ( 'NONE', #2553, #1943, #6167 ) ;
#2636=FACE_BOUND ( 'NONE', #2859, .T. ) ;
#2637=VERTEX_POINT ( 'NONE', #7658 ) ;
#2640=FACE_OUTER_BOUND ( 'NONE', #1758, .T. ) ;
#2641=AXIS2_PLACEMENT_3D ( 'NONE', #5896, #1076, #400 ) ;
#2642=CARTESIAN_POINT ( 'NONE',  ( 296.6025403784439050, 90.00000000000001421, 12.50000000000000000 ) ) ;
#2645=CARTESIAN_POINT ( 'NONE',  ( 296.6025403784439050, 0.000000000000000000, 12.50000000000000000 ) ) ;
#2649=EDGE_CURVE ( 'NONE', #2853, #5178, #6457, .T. ) ;
#2656=DIRECTION ( 'NONE',  ( -0.000000000000000000, -0.000000000000000000, -1.000000000000000000 ) ) ;
#2664=ORIENTED_EDGE ( 'NONE', *, *, #3323, .T. ) ;
#2665=VECTOR ( 'NONE', #7419, 1000.000000000000000 ) ;
#2678=DIRECTION ( 'NONE',  ( -0.000000000000000000, -0.000000000000000000, -1.000000000000000000 ) ) ;
#2679=CARTESIAN_POINT ( 'NONE',  ( 46.25000000000002842, 0.000000000000000000, 195.5000000000000000 ) ) ;
#2681=DIRECTION ( 'NONE',  ( 0.000000000000000000, -0.000000000000000000, -1.000000000000000000 ) ) ;
#2684=CARTESIAN_POINT ( 'NONE',  ( 3.592258498106024636E-14, 75.00000000000019895, 12.50000000000000000 ) ) ;
#2686=ORIENTED_EDGE ( 'NONE', *, *, #7323, .F. ) ;
#2687=DIRECTION ( 'NONE',  ( -1.000000000000000000, 0.000000000000000000, 0.000000000000000000 ) ) ;
#2689=ORIENTED_EDGE ( 'NONE', *, *, #4334, .T. ) ;
#2692=DIRECTION ( 'NONE',  ( -2.960594732333750117E-15, 1.000000000000000000, 0.000000000000000000 ) ) ;
#2695=CARTESIAN_POINT ( 'NONE',  ( 296.6025403784437913, 137.4999999999999716, 12.50000000000000000 ) ) ;
#2696=CARTESIAN_POINT ( 'NONE',  ( -37.49999999999992184, 111.9999999999999289, 130.0000000000000000 ) ) ;
#2701=ORIENTED_EDGE ( 'NONE', *, *, #1322, .T. ) ;
#2703=CARTESIAN_POINT ( 'NONE',  ( -7.184516996212029076E-14, 149.9999999999998295, 12.50000000000000000 ) ) ;
#2704=ORIENTED_EDGE ( 'NONE', *, *, #2580, .F. ) ;
#2707=DIRECTION ( 'NONE',  ( -0.000000000000000000, -0.000000000000000000, -1.000000000000000000 ) ) ;
#2709=ORIENTED_EDGE ( 'NONE', *, *, #5627, .F. ) ;
#2715=EDGE_LOOP ( 'NONE', ( #2622, #4121, #6142, #2686 ) ) ;
#2721=EDGE_CURVE ( 'NONE', #6773, #3816, #6660, .T. ) ;
#2723=CARTESIAN_POINT ( 'NONE',  ( -31.24999999999997158, 177.4999999999999432, 130.0000000000000000 ) ) ;
#2727=EDGE_CURVE ( 'NONE', #4433, #1919, #4686, .T. ) ;
#2728=CARTESIAN_POINT ( 'NONE',  ( 296.6025403784439050, 75.00000000000007105, 12.50000000000000000 ) ) ;
#2729=CARTESIAN_POINT ( 'NONE',  ( 42.50000000000000711, 177.5000000000000000, 0.000000000000000000 ) ) ;
#2731=ADVANCED_FACE ( 'NONE', ( #2897 ), #3533, .F. ) ;
#2739=CIRCLE ( 'NONE', #4775, 30.00000000000000000 ) ;
#2741=LINE ( 'NONE', #1017, #1857 ) ;
#2742=VECTOR ( 'NONE', #4506, 1000.000000000000000 ) ;
#2746=DIRECTION ( 'NONE',  ( 2.960594732333750117E-15, -1.000000000000000000, 0.000000000000000000 ) ) ;
#2747=LINE ( 'NONE', #4021, #3381 ) ;
#2751=ORIENTED_EDGE ( 'NONE', *, *, #3784, .T. ) ;
#2753=CIRCLE ( 'NONE', #4405, 32.75000000000000000 ) ;
#2755=VECTOR ( 'NONE', #2197, 1000.000000000000000 ) ;
#2756=FACE_OUTER_BOUND ( 'NONE', #238, .T. ) ;
#2758=ORIENTED_EDGE ( 'NONE', *, *, #3855, .T. ) ;
#2759=FACE_OUTER_BOUND ( 'NONE', #7413, .T. ) ;
#2760=CARTESIAN_POINT ( 'NONE',  ( 42.08354679051384295, 47.50000000000003553, 12.55124306091975583 ) ) ;
#2761=CARTESIAN_POINT ( 'NONE',  ( 0.000000000000000000, 177.4999999999999432, 12.50000000000000000 ) ) ;
#2763=CIRCLE ( 'NONE', #7249, 5.000000000000004441 ) ;
#2765=DIRECTION ( 'NONE',  ( 1.000000000000000000, 0.000000000000000000, 0.000000000000000000 ) ) ;
#2766=VERTEX_POINT ( 'NONE', #4726 ) ;
#2768=ORIENTED_EDGE ( 'NONE', *, *, #5420, .T. ) ;
#2770=CARTESIAN_POINT ( 'NONE',  ( -31.24999999999997158, 144.7499999999999432, 130.0000000000000000 ) ) ;
#2775=EDGE_CURVE ( 'NONE', #5735, #3550, #7143, .T. ) ;
#2780=CARTESIAN_POINT ( 'NONE',  ( 42.50000000000000000, 42.50000000000003553, 0.000000000000000000 ) ) ;
#2782=CARTESIAN_POINT ( 'NONE',  ( 46.25000000000002842, 47.50000000000003553, 130.0000000000000000 ) ) ;
#2783=ADVANCED_FACE ( 'NONE', ( #1043 ), #2938, .T. ) ;
#2785=DIRECTION ( 'NONE',  ( 4.270088556250607616E-16, 1.000000000000000000, 0.000000000000000000 ) ) ;
#2787=ORIENTED_EDGE ( 'NONE', *, *, #6280, .F. ) ;
#2793=EDGE_CURVE ( 'NONE', #5569, #1300, #4164, .T. ) ;
#2795=AXIS2_PLACEMENT_3D ( 'NONE', #4505, #381, #6316 ) ;
#2796=DIRECTION ( 'NONE',  ( 0.000000000000000000, -0.000000000000000000, -1.000000000000000000 ) ) ;
#2802=DIRECTION ( 'NONE',  ( -4.789677997474686366E-16, -1.000000000000000000, 0.000000000000000000 ) ) ;
#2804=AXIS2_PLACEMENT_3D ( 'NONE', #1258, #6153, #1296 ) ;
#2805=ORIENTED_EDGE ( 'NONE', *, *, #2775, .T. ) ;
#2809=AXIS2_PLACEMENT_3D ( 'NONE', #6413, #5736, #2159 ) ;
#2817=VECTOR ( 'NONE', #5732, 1000.000000000000000 ) ;
#2818=ORIENTED_EDGE ( 'NONE', *, *, #2125, .T. ) ;
#2823=EDGE_CURVE ( 'NONE', #5267, #3802, #115, .T. ) ;
#2828=ORIENTED_EDGE ( 'NONE', *, *, #1346, .T. ) ;
#2829=LINE ( 'NONE', #380, #1623 ) ;
#2830=CARTESIAN_POINT ( 'NONE',  ( 2.775557561562891351E-14, 225.0000000000000284, 12.50000000000000000 ) ) ;
#2833=DIRECTION ( 'NONE',  ( 1.000000000000000000, 0.000000000000000000, 0.000000000000000000 ) ) ;
#2837=ORIENTED_EDGE ( 'NONE', *, *, #5185, .F. ) ;
#2838=VERTEX_POINT ( 'NONE', #6251 ) ;
#2839=( NAMED_UNIT ( * ) SI_UNIT ( $, .STERADIAN. ) SOLID_ANGLE_UNIT ( ) );
#2840=ORIENTED_EDGE ( 'NONE', *, *, #4499, .T. ) ;
#2845=EDGE_LOOP ( 'NONE', ( #4840, #487, #2525, #4909 ) ) ;
#2851=ORIENTED_EDGE ( 'NONE', *, *, #374, .T. ) ;
#2853=VERTEX_POINT ( 'NONE', #1282 ) ;
#2854=CYLINDRICAL_SURFACE ( 'NONE', #2286, 65.50000000000000000 ) ;
#2856=DIRECTION ( 'NONE',  ( -0.5000000000000002220, -0.8660254037844384856, 0.000000000000000000 ) ) ;
#2859=EDGE_LOOP ( 'NONE', ( #7283, #3113 ) ) ;
#2863=PLANE ( 'NONE',  #2210 ) ;
#2864=CARTESIAN_POINT ( 'NONE',  ( 291.6025403784439050, 90.00000000000001421, 0.000000000000000000 ) ) ;
#2876=VERTEX_POINT ( 'NONE', #2599 ) ;
#2877=EDGE_CURVE ( 'NONE', #4540, #3234, #5614, .T. ) ;
#2878=ORIENTED_EDGE ( 'NONE', *, *, #7730, .F. ) ;
#2879=CARTESIAN_POINT ( 'NONE',  ( 412.5000000000000568, 80.00000000000001421, 0.000000000000000000 ) ) ;
#2881=CYLINDRICAL_SURFACE ( 'NONE', #3130, 5.000000000000004441 ) ;
#2882=ADVANCED_FACE ( 'NONE', ( #2522 ), #1874, .F. ) ;
#2885=DIRECTION ( 'NONE',  ( -0.000000000000000000, -0.000000000000000000, -1.000000000000000000 ) ) ;
#2887=AXIS2_PLACEMENT_3D ( 'NONE', #7457, #5494, #1917 ) ;
#2891=LINE ( 'NONE', #3006, #3958 ) ;
#2892=ORIENTED_EDGE ( 'NONE', *, *, #6722, .F. ) ;
#2894=ORIENTED_EDGE ( 'NONE', *, *, #2342, .F. ) ;
#2895=CARTESIAN_POINT ( 'NONE',  ( 200.0000000000000000, 0.000000000000000000, 12.50000000000000000 ) ) ;
#2897=FACE_OUTER_BOUND ( 'NONE', #7287, .T. ) ;
#2900=VERTEX_POINT ( 'NONE', #1394 ) ;
#2902=DIRECTION ( 'NONE',  ( -0.000000000000000000, -0.000000000000000000, -1.000000000000000000 ) ) ;
#2904=DIRECTION ( 'NONE',  ( -0.000000000000000000, 0.000000000000000000, -1.000000000000000000 ) ) ;
#2905=LINE ( 'NONE', #615, #6706 ) ;
#2909=DIRECTION ( 'NONE',  ( -0.000000000000000000, 0.000000000000000000, -1.000000000000000000 ) ) ;
#2912=ORIENTED_EDGE ( 'NONE', *, *, #7394, .T. ) ;
#2913=CARTESIAN_POINT ( 'NONE',  ( -37.49999999999992184, 112.5000000000000142, 195.4980915752512658 ) ) ;
#2916=FACE_BOUND ( 'NONE', #647, .T. ) ;
#2919=EDGE_CURVE ( 'NONE', #2226, #4382, #55, .T. ) ;
#2923=CARTESIAN_POINT ( 'NONE',  ( 296.6025403784437913, 142.5000000000000000, 17.49999999999998934 ) ) ;
#2930=CARTESIAN_POINT ( 'NONE',  ( 296.6025403784437913, 82.50000000000004263, 17.49999999999998934 ) ) ;
#2935=DIRECTION ( 'NONE',  ( -0.000000000000000000, 0.000000000000000000, 1.000000000000000000 ) ) ;
#2938=PLANE ( 'NONE',  #6215 ) ;
#2947=CARTESIAN_POINT ( 'NONE',  ( 353.4483633286965301, 75.00000000000004263, 138.3903618369216417 ) ) ;
#2949=AXIS2_PLACEMENT_3D ( 'NONE', #5852, #309, #2765 ) ;
#2950=AXIS2_PLACEMENT_3D ( 'NONE', #6224, #1808, #572 ) ;
#2952=CARTESIAN_POINT ( 'NONE',  ( 200.0000000000000000, 0.000000000000000000, 12.50000000000000000 ) ) ;
#2960=PRODUCT_DEFINITION_CONTEXT ( 'detailed design', #6798, 'design' ) ;
#2963=EDGE_LOOP ( 'NONE', ( #3159, #7017, #95, #5411, #1744, #7497, #2689 ) ) ;
#2967=CARTESIAN_POINT ( 'NONE',  ( -12.49999999999996803, 225.0000000000000284, 12.50000000000000000 ) ) ;
#2970=EDGE_LOOP ( 'NONE', ( #3840, #6213, #73, #7376 ) ) ;
#2973=VERTEX_POINT ( 'NONE', #1514 ) ;
#2974=LINE ( 'NONE', #6776, #7020 ) ;
#2975=CARTESIAN_POINT ( 'NONE',  ( 162.4999999999999432, 187.4999999999999716, 12.50000000000000000 ) ) ;
#2977=VERTEX_POINT ( 'NONE', #7531 ) ;
#2978=ORIENTED_EDGE ( 'NONE', *, *, #5093, .T. ) ;
#2979=EDGE_CURVE ( 'NONE', #2146, #6485, #4598, .T. ) ;
#2981=DIRECTION ( 'NONE',  ( -0.000000000000000000, -0.000000000000000000, -1.000000000000000000 ) ) ;
#2983=CARTESIAN_POINT ( 'NONE',  ( 286.6025403784437913, 0.000000000000000000, 12.50000000000000000 ) ) ;
#2985=DIRECTION ( 'NONE',  ( -4.237492460401359023E-16, -1.000000000000000000, 0.000000000000000000 ) ) ;
#2987=EDGE_CURVE ( 'NONE', #2, #1820, #7608, .T. ) ;
#2988=EDGE_CURVE ( 'NONE', #2325, #5081, #2113, .T. ) ;
#2989=FACE_OUTER_BOUND ( 'NONE', #3043, .T. ) ;
#2991=DIRECTION ( 'NONE',  ( 1.000000000000000000, 0.000000000000000000, 0.000000000000000000 ) ) ;
#2994=CARTESIAN_POINT ( 'NONE',  ( 0.000000000000000000, 47.50000000000009237, 12.50000000000000000 ) ) ;
#2997=AXIS2_PLACEMENT_3D ( 'NONE', #7430, #1171, #1925 ) ;
#3001=CYLINDRICAL_SURFACE ( 'NONE', #2487, 12.50000000000001066 ) ;
#3003=AXIS2_PLACEMENT_3D ( 'NONE', #2994, #4863, #7909 ) ;
#3005=VERTEX_POINT ( 'NONE', #7088 ) ;
#3006=CARTESIAN_POINT ( 'NONE',  ( 47.50000000000000711, 0.000000000000000000, 0.000000000000000000 ) ) ;
#3007=ORIENTED_EDGE ( 'NONE', *, *, #3636, .F. ) ;
#3013=DIRECTION ( 'NONE',  ( -0.000000000000000000, -0.000000000000000000, -1.000000000000000000 ) ) ;
#3018=VERTEX_POINT ( 'NONE', #2642 ) ;
#3021=AXIS2_PLACEMENT_3D ( 'NONE', #6755, #1739, #1819 ) ;
#3025=DIRECTION ( 'NONE',  ( -1.000000000000000000, -1.261617073437677999E-16, 0.000000000000000000 ) ) ;
#3027=EDGE_CURVE ( 'NONE', #2041, #5081, #4923, .T. ) ;
#3032=CARTESIAN_POINT ( 'NONE',  ( 335.4891275541129971, 142.5000000000000000, 174.3961449365926626 ) ) ;
#3042=LINE ( 'NONE', #2251, #1848 ) ;
#3043=EDGE_LOOP ( 'NONE', ( #2442, #1026, #2828, #3398 ) ) ;
#3045=CYLINDRICAL_SURFACE ( 'NONE', #5181, 37.50000000000000000 ) ;
#3046=ADVANCED_FACE ( 'NONE', ( #5849, #4557 ), #7012, .T. ) ;
#3051=VERTEX_POINT ( 'NONE', #7691 ) ;
#3056=AXIS2_PLACEMENT_3D ( 'NONE', #2119, #6940, #4523 ) ;
#3059=ORIENTED_EDGE ( 'NONE', *, *, #6061, .F. ) ;
#3061=VECTOR ( 'NONE', #336, 1000.000000000000000 ) ;
#3066=DIRECTION ( 'NONE',  ( -1.000000000000000000, 0.000000000000000000, 0.000000000000000000 ) ) ;
#3067=DIRECTION ( 'NONE',  ( -0.000000000000000000, -0.000000000000000000, -1.000000000000000000 ) ) ;
#3073=AXIS2_PLACEMENT_3D ( 'NONE', #7094, #5894, #4040 ) ;
#3079=ADVANCED_FACE ( 'NONE', ( #7570 ), #2072, .F. ) ;
#3080=ORIENTED_EDGE ( 'NONE', *, *, #4999, .F. ) ;
#3083=EDGE_CURVE ( 'NONE', #3773, #4917, #6410, .T. ) ;
#3087=ORIENTED_EDGE ( 'NONE', *, *, #6722, .T. ) ;
#3088=CARTESIAN_POINT ( 'NONE',  ( 2.775557561562891351E-14, 225.0000000000000284, 12.50000000000000000 ) ) ;
#3089=ORIENTED_EDGE ( 'NONE', *, *, #470, .T. ) ;
#3090=EDGE_CURVE ( 'NONE', #2269, #5006, #5808, .T. ) ;
#3094=VERTEX_POINT ( 'NONE', #3560 ) ;
#3096=DIRECTION ( 'NONE',  ( 4.237492460401360996E-16, 1.000000000000000000, -1.694996984160544398E-15 ) ) ;
#3103=CARTESIAN_POINT ( 'NONE',  ( 286.6025403784439050, 0.000000000000000000, 12.50000000000000000 ) ) ;
#3108=DIRECTION ( 'NONE',  ( 0.000000000000000000, -1.694996984160544398E-15, 1.000000000000000000 ) ) ;
#3109=LINE ( 'NONE', #5545, #2523 ) ;
#3113=ORIENTED_EDGE ( 'NONE', *, *, #1644, .T. ) ;
#3116=DIRECTION ( 'NONE',  ( 0.000000000000000000, -1.000000000000000000, 0.000000000000000000 ) ) ;
#3118=CARTESIAN_POINT ( 'NONE',  ( -37.49999999999992184, 111.9999999999999289, 130.0000000000000000 ) ) ;
#3119=CARTESIAN_POINT ( 'NONE',  ( 42.50000000000000000, 42.50000000000003553, 12.50000000000000000 ) ) ;
#3122=AXIS2_PLACEMENT_3D ( 'NONE', #6065, #6188, #573 ) ;
#3123=EDGE_CURVE ( 'NONE', #3802, #1919, #3782, .T. ) ;
#3130=AXIS2_PLACEMENT_3D ( 'NONE', #6681, #6533, #4150 ) ;
#3133=VERTEX_POINT ( 'NONE', #1753 ) ;
#3135=EDGE_LOOP ( 'NONE', ( #7851, #7847, #2489, #3174 ) ) ;
#3136=ORIENTED_EDGE ( 'NONE', *, *, #5380, .T. ) ;
#3142=DIRECTION ( 'NONE',  ( -1.000000000000000000, -4.789677997474691297E-16, 0.000000000000000000 ) ) ;
#3144=VECTOR ( 'NONE', #3013, 1000.000000000000000 ) ;
#3148=DIRECTION ( 'NONE',  ( 1.000000000000000000, 0.000000000000000000, 0.000000000000000000 ) ) ;
#3149=CYLINDRICAL_SURFACE ( 'NONE', #4204, 12.50000000000001066 ) ;
#3159=ORIENTED_EDGE ( 'NONE', *, *, #5595, .T. ) ;
#3165=CARTESIAN_POINT ( 'NONE',  ( 62.50000000000009948, 144.7499999999999147, 130.0000000000000000 ) ) ;
#3166=AXIS2_PLACEMENT_3D ( 'NONE', #3946, #7040, #4617 ) ;
#3168=EDGE_CURVE ( 'NONE', #1999, #6360, #7619, .T. ) ;
#3173=ORIENTED_EDGE ( 'NONE', *, *, #5870, .T. ) ;
#3174=ORIENTED_EDGE ( 'NONE', *, *, #3815, .F. ) ;
#3179=DIRECTION ( 'NONE',  ( 1.000000000000000000, 0.000000000000000000, 0.000000000000000000 ) ) ;
#3180=LINE ( 'NONE', #81, #6911 ) ;
#3184=CIRCLE ( 'NONE', #7910, 74.99999999999995737 ) ;
#3186=FACE_OUTER_BOUND ( 'NONE', #2715, .T. ) ;
#3189=CARTESIAN_POINT ( 'NONE',  ( 162.4999999999999432, 187.4999999999999716, 0.000000000000000000 ) ) ;
#3194=ORIENTED_EDGE ( 'NONE', *, *, #2649, .F. ) ;
#3196=CARTESIAN_POINT ( 'NONE',  ( 286.6025403784439050, 75.00000000000002842, 12.50000000000000000 ) ) ;
#3197=EDGE_CURVE ( 'NONE', #916, #7160, #5364, .T. ) ;
#3200=DIRECTION ( 'NONE',  ( 0.000000000000000000, -1.000000000000000000, 0.000000000000000000 ) ) ;
#3201=CIRCLE ( 'NONE', #7300, 12.50000000000001066 ) ;
#3203=ORIENTED_EDGE ( 'NONE', *, *, #168, .T. ) ;
#3206=LINE ( 'NONE', #3279, #6991 ) ;
#3212=ORIENTED_EDGE ( 'NONE', *, *, #6502, .F. ) ;
#3213=ORIENTED_EDGE ( 'NONE', *, *, #3123, .T. ) ;
#3216=ORIENTED_EDGE ( 'NONE', *, *, #3327, .T. ) ;
#3217=LINE ( 'NONE', #2496, #580 ) ;
#3229=EDGE_LOOP ( 'NONE', ( #4919, #751, #3173, #5367 ) ) ;
#3233=DIRECTION ( 'NONE',  ( 0.000000000000000000, 0.000000000000000000, 1.000000000000000000 ) ) ;
#3234=VERTEX_POINT ( 'NONE', #4835 ) ;
#3240=ORIENTED_EDGE ( 'NONE', *, *, #7582, .T. ) ;
#3246=ORIENTED_EDGE ( 'NONE', *, *, #311, .T. ) ;
#3247=LINE ( 'NONE', #198, #3557 ) ;
#3248=LINE ( 'NONE', #315, #6832 ) ;
#3250=ORIENTED_EDGE ( 'NONE', *, *, #2987, .T. ) ;
#3255=DIRECTION ( 'NONE',  ( 1.000000000000000000, 0.000000000000000000, 0.000000000000000000 ) ) ;
#3257=DIRECTION ( 'NONE',  ( 0.000000000000000000, 0.000000000000000000, 1.000000000000000000 ) ) ;
#3265=DIRECTION ( 'NONE',  ( 1.000000000000000000, -0.000000000000000000, 0.000000000000000000 ) ) ;
#3267=DIRECTION ( 'NONE',  ( 0.000000000000000000, 0.000000000000000000, -1.000000000000000000 ) ) ;
#3271=ADVANCED_FACE ( 'NONE', ( #7450 ), #3045, .T. ) ;
#3272=AXIS2_PLACEMENT_3D ( 'NONE', #3591, #2386, #5472 ) ;
#3278=EDGE_LOOP ( 'NONE', ( #7764, #591 ) ) ;
#3279=CARTESIAN_POINT ( 'NONE',  ( 182.4759526419164217, -105.3525403784438907, 12.50000000000000000 ) ) ;
#3280=FACE_BOUND ( 'NONE', #6481, .T. ) ;
#3281=FACE_OUTER_BOUND ( 'NONE', #6557, .T. ) ;
#3284=VERTEX_POINT ( 'NONE', #4351 ) ;
#3285=AXIS2_PLACEMENT_3D ( 'NONE', #347, #987, #5190 ) ;
#3287=ORIENTED_EDGE ( 'NONE', *, *, #765, .T. ) ;
#3291=CARTESIAN_POINT ( 'NONE',  ( -26.24999999999997158, 177.4999999999999432, 17.50000000000001421 ) ) ;
#3307=CIRCLE ( 'NONE', #5091, 12.50000000000001066 ) ;
#3311=EDGE_CURVE ( 'NONE', #2601, #3051, #1731, .T. ) ;
#3314=AXIS2_PLACEMENT_3D ( 'NONE', #2761, #6535, #1551 ) ;
#3316=EDGE_CURVE ( 'NONE', #3491, #916, #1224, .T. ) ;
#3318=ADVANCED_FACE ( 'NONE', ( #5524 ), #746, .F. ) ;
#3323=EDGE_CURVE ( 'NONE', #4316, #1036, #668, .T. ) ;
#3325=DIRECTION ( 'NONE',  ( -4.237492460401359023E-16, -1.000000000000000000, 0.000000000000000000 ) ) ;
#3327=EDGE_CURVE ( 'NONE', #4382, #5563, #3532, .T. ) ;
#3330=CARTESIAN_POINT ( 'NONE',  ( 232.4759526419164786, -18.74999999999998934, 0.000000000000000000 ) ) ;
#3342=CARTESIAN_POINT ( 'NONE',  ( 232.4759526419164217, 243.7500000000000000, 12.50000000000000000 ) ) ;
#3344=DIRECTION ( 'NONE',  ( -4.789677997474686366E-16, -1.000000000000000000, -0.000000000000000000 ) ) ;
#3347=DIRECTION ( 'NONE',  ( -1.000000000000000000, 0.000000000000000000, 0.000000000000000000 ) ) ;
#3357=DIRECTION ( 'NONE',  ( 0.000000000000000000, 1.000000000000000000, 0.000000000000000000 ) ) ;
#3358=FACE_OUTER_BOUND ( 'NONE', #679, .T. ) ;
#3360=CARTESIAN_POINT ( 'NONE',  ( -27.49999999999989342, 187.4999999999999432, 12.50000000000000000 ) ) ;
#3361=ADVANCED_FACE ( 'NONE', ( #5029 ), #4872, .T. ) ;
#3366=CARTESIAN_POINT ( 'NONE',  ( 412.5000000000000568, 75.00000000000001421, 12.50000000000000000 ) ) ;
#3368=CARTESIAN_POINT ( 'NONE',  ( -31.24999999999997158, 47.50000000000009237, 17.50000000000001421 ) ) ;
#3369=LINE ( 'NONE', #3969, #5034 ) ;
#3374=CARTESIAN_POINT ( 'NONE',  ( 0.000000000000000000, 177.5000000000000000, 130.0000000000000000 ) ) ;
#3377=DIRECTION ( 'NONE',  ( -4.789677997474686366E-16, -1.000000000000000000, -0.000000000000000000 ) ) ;
#3379=EDGE_CURVE ( 'NONE', #1919, #3284, #7371, .T. ) ;
#3381=VECTOR ( 'NONE', #6923, 1000.000000000000000 ) ;
#3384=ORIENTED_EDGE ( 'NONE', *, *, #2823, .T. ) ;
#3388=FACE_BOUND ( 'NONE', #4479, .T. ) ;
#3393=EDGE_CURVE ( 'NONE', #1872, #5244, #2513, .T. ) ;
#3398=ORIENTED_EDGE ( 'NONE', *, *, #7726, .T. ) ;
#3400=DIRECTION ( 'NONE',  ( 4.789677997474685380E-16, 1.000000000000000000, 0.000000000000000000 ) ) ;
#3407=FACE_OUTER_BOUND ( 'NONE', #5292, .T. ) ;
#3410=CARTESIAN_POINT ( 'NONE',  ( 162.5000000000000000, 37.50000000000006395, 12.50000000000000000 ) ) ;
#3411=DIRECTION ( 'NONE',  ( -0.000000000000000000, 0.000000000000000000, 1.000000000000000000 ) ) ;
#3416=EDGE_CURVE ( 'NONE', #6617, #393, #2741, .T. ) ;
#3420=STYLED_ITEM('',(#7941),#4361);
#3429=DIRECTION ( 'NONE',  ( -0.000000000000000000, -0.000000000000000000, -1.000000000000000000 ) ) ;
#3431=CARTESIAN_POINT ( 'NONE',  ( 0.000000000000000000, 187.4999999999999432, 12.50000000000000000 ) ) ;
#3433=ORIENTED_EDGE ( 'NONE', *, *, #7478, .F. ) ;
#3438=VECTOR ( 'NONE', #3724, 1000.000000000000000 ) ;
#3441=ADVANCED_FACE ( 'NONE', ( #4574 ), #7034, .F. ) ;
#3442=CARTESIAN_POINT ( 'NONE',  ( 412.4999999999998863, 82.50000000000004263, 155.0000000000000000 ) ) ;
#3446=DIRECTION ( 'NONE',  ( 1.000000000000000000, 0.000000000000000000, 0.000000000000000000 ) ) ;
#3447=AXIS2_PLACEMENT_3D ( 'NONE', #3959, #5613, #113 ) ;
#3449=ORIENTED_EDGE ( 'NONE', *, *, #1545, .F. ) ;
#3452=CIRCLE ( 'NONE', #2949, 37.50000000000000000 ) ;
#3453=CARTESIAN_POINT ( 'NONE',  ( 42.50000000000000711, 182.5000000000000000, 12.50000000000000000 ) ) ;
#3458=CARTESIAN_POINT ( 'NONE',  ( -7.184516996212029076E-14, 149.9999999999998295, 5.000000000000000000 ) ) ;
#3464=PLANE ( 'NONE',  #988 ) ;
#3466=LINE ( 'NONE', #2304, #2341 ) ;
#3467=DIRECTION ( 'NONE',  ( 0.000000000000000000, -1.000000000000000000, 0.000000000000000000 ) ) ;
#3470=EDGE_CURVE ( 'NONE', #1036, #3550, #5454, .T. ) ;
#3473=ORIENTED_EDGE ( 'NONE', *, *, #6012, .T. ) ;
#3475=CARTESIAN_POINT ( 'NONE',  ( -31.24999999999997158, 0.000000000000000000, 17.50000000000001421 ) ) ;
#3479=VERTEX_POINT ( 'NONE', #7113 ) ;
#3491=VERTEX_POINT ( 'NONE', #416 ) ;
#3492=DIRECTION ( 'NONE',  ( -0.000000000000000000, 0.000000000000000000, 1.000000000000000000 ) ) ;
#3493=VERTEX_POINT ( 'NONE', #2782 ) ;
#3494=CARTESIAN_POINT ( 'NONE',  ( 162.5000000000000000, 112.5000000000000142, 12.50000000000000000 ) ) ;
#3495=CARTESIAN_POINT ( 'NONE',  ( 296.6025403784439050, 0.000000000000000000, 0.000000000000000000 ) ) ;
#3498=ORIENTED_EDGE ( 'NONE', *, *, #7702, .T. ) ;
#3501=DIRECTION ( 'NONE',  ( 1.000000000000000000, 0.000000000000000000, 0.000000000000000000 ) ) ;
#3512=ORIENTED_EDGE ( 'NONE', *, *, #4046, .F. ) ;
#3514=AXIS2_PLACEMENT_3D ( 'NONE', #1811, #576, #5463 ) ;
#3516=ORIENTED_EDGE ( 'NONE', *, *, #6747, .T. ) ;
#3521=ORIENTED_EDGE ( 'NONE', *, *, #4531, .F. ) ;
#3526=EDGE_CURVE ( 'NONE', #2477, #3534, #2763, .T. ) ;
#3527=DIRECTION ( 'NONE',  ( 0.8660254037844385966, 0.5000000000000003331, -0.000000000000000000 ) ) ;
#3528=ORIENTED_EDGE ( 'NONE', *, *, #4550, .F. ) ;
#3529=CARTESIAN_POINT ( 'NONE',  ( 182.4759526419164217, -105.3525403784438907, 0.000000000000000000 ) ) ;
#3530=EDGE_LOOP ( 'NONE', ( #4481, #2118, #1243, #5021 ) ) ;
#3532=CIRCLE ( 'NONE', #62, 65.50000000000000000 ) ;
#3533=CYLINDRICAL_SURFACE ( 'NONE', #6856, 12.49999999999999467 ) ;
#3534=VERTEX_POINT ( 'NONE', #577 ) ;
#3537=EDGE_CURVE ( 'NONE', #3491, #2126, #2377, .T. ) ;
#3540=CARTESIAN_POINT ( 'NONE',  ( 42.50000000000000000, 47.50000000000003553, 12.50000000000000000 ) ) ;
#3541=CYLINDRICAL_SURFACE ( 'NONE', #3642, 32.75000000000001421 ) ;
#3542=CIRCLE ( 'NONE', #7629, 32.75000000000000000 ) ;
#3543=DIRECTION ( 'NONE',  ( 0.000000000000000000, -0.000000000000000000, -1.000000000000000000 ) ) ;
#3549=DIRECTION ( 'NONE',  ( -0.000000000000000000, -0.000000000000000000, -1.000000000000000000 ) ) ;
#3550=VERTEX_POINT ( 'NONE', #1771 ) ;
#3551=AXIS2_PLACEMENT_3D ( 'NONE', #7028, #3894, #6342 ) ;
#3554=EDGE_CURVE ( 'NONE', #5735, #3493, #4217, .T. ) ;
#3555=EDGE_LOOP ( 'NONE', ( #524, #6760 ) ) ;
#3556=DIRECTION ( 'NONE',  ( 0.000000000000000000, 1.000000000000000000, 0.000000000000000000 ) ) ;
#3557=VECTOR ( 'NONE', #3885, 1000.000000000000000 ) ;
#3560=CARTESIAN_POINT ( 'NONE',  ( 46.25000000000002842, 112.5000000000000142, 195.4980915752512658 ) ) ;
#3563=CIRCLE ( 'NONE', #4576, 12.49999999999999467 ) ;
#3570=AXIS2_PLACEMENT_3D ( 'NONE', #2703, #7555, #4417 ) ;
#3572=CARTESIAN_POINT ( 'NONE',  ( 12.50000000000000000, 1.530808498934191521E-15, 12.50000000000000000 ) ) ;
#3574=ORIENTED_EDGE ( 'NONE', *, *, #237, .T. ) ;
#3578=LINE ( 'NONE', #1767, #2008 ) ;
#3580=LINE ( 'NONE', #3540, #3783 ) ;
#3582=VECTOR ( 'NONE', #7181, 1000.000000000000000 ) ;
#3585=EDGE_CURVE ( 'NONE', #2101, #2637, #715, .T. ) ;
#3586=CARTESIAN_POINT ( 'NONE',  ( 52.50000000000000711, 113.0000000000000426, 130.0000000000000000 ) ) ;
#3591=CARTESIAN_POINT ( 'NONE',  ( 412.4999999999998863, 137.4999999999999716, 17.49999999999998934 ) ) ;
#3593=VERTEX_POINT ( 'NONE', #1040 ) ;
#3595=ORIENTED_EDGE ( 'NONE', *, *, #7679, .T. ) ;
#3596=DIRECTION ( 'NONE',  ( -1.000000000000000000, 0.000000000000000000, 0.000000000000000000 ) ) ;
#3604=AXIS2_PLACEMENT_3D ( 'NONE', #4471, #1466, #7526 ) ;
#3607=ORIENTED_EDGE ( 'NONE', *, *, #4728, .T. ) ;
#3609=FACE_BOUND ( 'NONE', #5698, .T. ) ;
#3611=EDGE_CURVE ( 'NONE', #1117, #1583, #5854, .T. ) ;
#3613=EDGE_LOOP ( 'NONE', ( #2440, #4322, #7734, #876 ) ) ;
#3625=CARTESIAN_POINT ( 'NONE',  ( 326.6025403784438481, 150.0000000000000568, 125.0000000000000000 ) ) ;
#3626=DIRECTION ( 'NONE',  ( 0.000000000000000000, -1.000000000000000000, 0.000000000000000000 ) ) ;
#3627=DIRECTION ( 'NONE',  ( -0.000000000000000000, -0.000000000000000000, -1.000000000000000000 ) ) ;
#3629=EDGE_CURVE ( 'NONE', #5360, #5569, #1233, .T. ) ;
#3630=DIRECTION ( 'NONE',  ( 1.000000000000000000, 0.000000000000000000, 0.000000000000000000 ) ) ;
#3631=ORIENTED_EDGE ( 'NONE', *, *, #6771, .T. ) ;
#3632=ORIENTED_EDGE ( 'NONE', *, *, #4092, .T. ) ;
#3633=DIRECTION ( 'NONE',  ( -1.000000000000000000, -2.960594732333750117E-15, 0.000000000000000000 ) ) ;
#3636=EDGE_CURVE ( 'NONE', #7566, #846, #442, .T. ) ;
#3642=AXIS2_PLACEMENT_3D ( 'NONE', #4856, #3663, #2985 ) ;
#3643=DIRECTION ( 'NONE',  ( 1.000000000000000000, 0.000000000000000000, 0.000000000000000000 ) ) ;
#3647=ORIENTED_EDGE ( 'NONE', *, *, #7243, .F. ) ;
#3648=DIRECTION ( 'NONE',  ( -4.789677997474686366E-16, -1.000000000000000000, -0.000000000000000000 ) ) ;
#3652=ORIENTED_EDGE ( 'NONE', *, *, #5473, .T. ) ;
#3653=EDGE_CURVE ( 'NONE', #4754, #5349, #204, .T. ) ;
#3656=EDGE_CURVE ( 'NONE', #7589, #792, #4638, .T. ) ;
#3657=DIRECTION ( 'NONE',  ( 1.000000000000000000, 0.000000000000000000, 0.000000000000000000 ) ) ;
#3659=VECTOR ( 'NONE', #2337, 1000.000000000000000 ) ;
#3662=DIRECTION ( 'NONE',  ( -0.000000000000000000, -0.000000000000000000, -1.000000000000000000 ) ) ;
#3663=DIRECTION ( 'NONE',  ( -1.000000000000000000, 4.270088556250607616E-16, -0.000000000000000000 ) ) ;
#3667=EDGE_CURVE ( 'NONE', #698, #1300, #5716, .T. ) ;
#3668=DIRECTION ( 'NONE',  ( 1.000000000000000000, -0.000000000000000000, -0.000000000000000000 ) ) ;
#3677=AXIS2_PLACEMENT_3D ( 'NONE', #6005, #3116, #3267 ) ;
#3680=DIRECTION ( 'NONE',  ( -1.000000000000000000, -0.000000000000000000, -0.000000000000000000 ) ) ;
#3682=DIRECTION ( 'NONE',  ( -0.4463453945640545872, 2.055455305587023282E-16, 0.8948607650084221543 ) ) ;
#3684=VERTEX_POINT ( 'NONE', #7096 ) ;
#3688=ORIENTED_EDGE ( 'NONE', *, *, #2988, .F. ) ;
#3689=ADVANCED_FACE ( 'NONE', ( #3407 ), #356, .T. ) ;
#3694=ORIENTED_EDGE ( 'NONE', *, *, #2085, .T. ) ;
#3695=FACE_BOUND ( 'NONE', #1360, .T. ) ;
#3697=VECTOR ( 'NONE', #2453, 1000.000000000000000 ) ;
#3699=ORIENTED_EDGE ( 'NONE', *, *, #6258, .F. ) ;
#3701=AXIS2_PLACEMENT_3D ( 'NONE', #402, #5286, #2353 ) ;
#3703=DIRECTION ( 'NONE',  ( 0.8948607650084221543, -4.286094916964204981E-16, 0.4463453945640545317 ) ) ;
#3708=AXIS2_PLACEMENT_3D ( 'NONE', #2196, #991, #7051 ) ;
#3710=DIRECTION ( 'NONE',  ( 1.000000000000000000, -0.000000000000000000, -0.000000000000000000 ) ) ;
#3712=VECTOR ( 'NONE', #6294, 1000.000000000000000 ) ;
#3717=CARTESIAN_POINT ( 'NONE',  ( -37.49999999999995026, 47.50000000000009237, 5.000000000000000000 ) ) ;
#3721=VERTEX_POINT ( 'NONE', #7781 ) ;
#3724=DIRECTION ( 'NONE',  ( -1.000000000000000000, -1.261617073437677999E-16, 0.000000000000000000 ) ) ;
#3728=ORIENTED_EDGE ( 'NONE', *, *, #1649, .F. ) ;
#3732=EDGE_LOOP ( 'NONE', ( #3059, #1674, #5738, #4044 ) ) ;
#3741=ORIENTED_EDGE ( 'NONE', *, *, #1834, .F. ) ;
#3746=LINE ( 'NONE', #4328, #2212 ) ;
#3754=EDGE_LOOP ( 'NONE', ( #3688, #3998, #353, #2892 ) ) ;
#3761=LINE ( 'NONE', #177, #5566 ) ;
#3762=EDGE_LOOP ( 'NONE', ( #2409, #6330, #3136, #1954, #3194, #2818, #1716, #3007, #7324, #6506, #7854, #6310, #3987, #1245, #285, #384, #6866, #3652, #4161, #5809, #7804, #3250, #4311, #6352, #1479, #4031 ) ) ;
#3769=ORIENTED_EDGE ( 'NONE', *, *, #5870, .F. ) ;
#3773=VERTEX_POINT ( 'NONE', #5729 ) ;
#3777=DIRECTION ( 'NONE',  ( 0.000000000000000000, -0.000000000000000000, -1.000000000000000000 ) ) ;
#3778=DIRECTION ( 'NONE',  ( 0.000000000000000000, -0.000000000000000000, -1.000000000000000000 ) ) ;
#3780=CIRCLE ( 'NONE', #953, 12.50000000000001066 ) ;
#3782=CIRCLE ( 'NONE', #316, 74.99999999999995737 ) ;
#3783=VECTOR ( 'NONE', #971, 1000.000000000000000 ) ;
#3784=EDGE_CURVE ( 'NONE', #481, #3051, #6890, .T. ) ;
#3786=CARTESIAN_POINT ( 'NONE',  ( 2.775557561562891351E-14, 262.5000000000000568, 12.50000000000000000 ) ) ;
#3789=DIRECTION ( 'NONE',  ( 0.000000000000000000, 0.000000000000000000, -1.000000000000000000 ) ) ;
#3790=VECTOR ( 'NONE', #7411, 1000.000000000000000 ) ;
#3791=ORIENTED_EDGE ( 'NONE', *, *, #4262, .F. ) ;
#3794=CARTESIAN_POINT ( 'NONE',  ( 412.5000000000002274, 1.221245327087672598E-12, 0.000000000000000000 ) ) ;
#3798=DIRECTION ( 'NONE',  ( -0.000000000000000000, -0.000000000000000000, -1.000000000000000000 ) ) ;
#3800=ORIENTED_EDGE ( 'NONE', *, *, #5093, .F. ) ;
#3802=VERTEX_POINT ( 'NONE', #6286 ) ;
#3805=DIRECTION ( 'NONE',  ( 0.000000000000000000, -1.000000000000000000, 0.000000000000000000 ) ) ;
#3807=EDGE_CURVE ( 'NONE', #3094, #3133, #6965, .T. ) ;
#3809=EDGE_CURVE ( 'NONE', #1399, #2876, #7416, .T. ) ;
#3814=LINE ( 'NONE', #6186, #1249 ) ;
#3815=EDGE_CURVE ( 'NONE', #3493, #3094, #1610, .T. ) ;
#3816=VERTEX_POINT ( 'NONE', #3917 ) ;
#3819=DIRECTION ( 'NONE',  ( -0.000000000000000000, -0.000000000000000000, -1.000000000000000000 ) ) ;
#3821=DIRECTION ( 'NONE',  ( 0.000000000000000000, 0.000000000000000000, -1.000000000000000000 ) ) ;
#3826=EDGE_LOOP ( 'NONE', ( #2188, #4142 ) ) ;
#3830=ORIENTED_EDGE ( 'NONE', *, *, #7440, .F. ) ;
#3832=CARTESIAN_POINT ( 'NONE',  ( -27.49999999999989342, 182.4999999999999432, 0.000000000000000000 ) ) ;
#3837=VECTOR ( 'NONE', #1510, 1000.000000000000000 ) ;
#3840=ORIENTED_EDGE ( 'NONE', *, *, #3629, .T. ) ;
#3847=LINE ( 'NONE', #5082, #3712 ) ;
#3848=ORIENTED_EDGE ( 'NONE', *, *, #6502, .T. ) ;
#3850=VERTEX_POINT ( 'NONE', #788 ) ;
#3853=CARTESIAN_POINT ( 'NONE',  ( 200.0000000000000000, -37.50000000000000711, 0.000000000000000000 ) ) ;
#3855=EDGE_CURVE ( 'NONE', #5478, #279, #3206, .T. ) ;
#3861=FACE_OUTER_BOUND ( 'NONE', #4688, .T. ) ;
#3862=CARTESIAN_POINT ( 'NONE',  ( 46.25000000000002842, 111.9999999999999005, 130.0000000000000000 ) ) ;
#3863=CARTESIAN_POINT ( 'NONE',  ( -32.49999999999990052, 177.4999999999999432, 5.000000000000000000 ) ) ;
#3867=ORIENTED_EDGE ( 'NONE', *, *, #3537, .F. ) ;
#3872=ORIENTED_EDGE ( 'NONE', *, *, #4966, .T. ) ;
#3874=CARTESIAN_POINT ( 'NONE',  ( 46.25000000000002842, 47.50000000000003553, 17.50000000000000000 ) ) ;
#3876=EDGE_CURVE ( 'NONE', #279, #846, #6323, .T. ) ;
#3879=DIRECTION ( 'NONE',  ( -1.000000000000000000, 0.000000000000000000, 0.000000000000000000 ) ) ;
#3884=ORIENTED_EDGE ( 'NONE', *, *, #1065, .F. ) ;
#3885=DIRECTION ( 'NONE',  ( 1.000000000000000000, -3.469446951953614189E-17, 0.000000000000000000 ) ) ;
#3893=AXIS2_PLACEMENT_3D ( 'NONE', #2501, #1332, #584 ) ;
#3894=DIRECTION ( 'NONE',  ( 1.000000000000000000, -0.000000000000000000, -0.000000000000000000 ) ) ;
#3896=DIRECTION ( 'NONE',  ( -1.000000000000000000, 0.000000000000000000, 0.000000000000000000 ) ) ;
#3898=ADVANCED_FACE ( 'NONE', ( #5770, #269 ), #2192, .F. ) ;
#3900=AXIS2_PLACEMENT_3D ( 'NONE', #5773, #4516, #1473 ) ;
#3903=EDGE_CURVE ( 'NONE', #3018, #2853, #906, .T. ) ;
#3908=VECTOR ( 'NONE', #4673, 1000.000000000000000 ) ;
#3911=EDGE_LOOP ( 'NONE', ( #7105, #7874 ) ) ;
#3913=ADVANCED_FACE ( 'NONE', ( #7724 ), #7085, .T. ) ;
#3917=CARTESIAN_POINT ( 'NONE',  ( -27.49999999999994671, 37.50000000000008527, 0.000000000000000000 ) ) ;
#3919=DIRECTION ( 'NONE',  ( -1.000000000000000000, 4.270088556250607616E-16, -0.000000000000000000 ) ) ;
#3921=EDGE_CURVE ( 'NONE', #7220, #5242, #973, .T. ) ;
#3926=ORIENTED_EDGE ( 'NONE', *, *, #5670, .T. ) ;
#3932=AXIS2_PLACEMENT_3D ( 'NONE', #3625, #4221, #2991 ) ;
#3935=CARTESIAN_POINT ( 'NONE',  ( 353.4483633286965301, 150.0000000000000284, 138.3903618369216417 ) ) ;
#3937=DIRECTION ( 'NONE',  ( 1.000000000000000000, 0.000000000000000000, 0.000000000000000000 ) ) ;
#3940=VECTOR ( 'NONE', #1402, 1000.000000000000000 ) ;
#3944=AXIS2_PLACEMENT_3D ( 'NONE', #5347, #5991, #2785 ) ;
#3946=CARTESIAN_POINT ( 'NONE',  ( 199.9999999999998863, 225.0000000000000284, 12.50000000000000000 ) ) ;
#3947=CARTESIAN_POINT ( 'NONE',  ( 2.775557561562891351E-14, 225.0000000000000284, 0.000000000000000000 ) ) ;
#3950=CARTESIAN_POINT ( 'NONE',  ( 2.775557561562891351E-14, 225.0000000000000284, 12.50000000000000000 ) ) ;
#3952=ADVANCED_FACE ( 'NONE', ( #2759 ), #7175, .T. ) ;
#3957=CARTESIAN_POINT ( 'NONE',  ( 2.775557561562891351E-14, 262.5000000000000568, 0.000000000000000000 ) ) ;
#3958=VECTOR ( 'NONE', #1712, 1000.000000000000000 ) ;
#3959=CARTESIAN_POINT ( 'NONE',  ( 296.6025403784437913, 0.000000000000000000, 12.50000000000000000 ) ) ;
#3961=CARTESIAN_POINT ( 'NONE',  ( 200.0000000000000000, 0.000000000000000000, 0.000000000000000000 ) ) ;
#3964=ORIENTED_EDGE ( 'NONE', *, *, #7639, .F. ) ;
#3969=CARTESIAN_POINT ( 'NONE',  ( -37.50000000000000000, 4.592427351555481498E-15, 12.50000000000000000 ) ) ;
#3976=FACE_OUTER_BOUND ( 'NONE', #1958, .T. ) ;
#3979=EDGE_LOOP ( 'NONE', ( #4027, #1145, #662, #5840 ) ) ;
#3984=CARTESIAN_POINT ( 'NONE',  ( 0.000000000000000000, 113.0000000000000426, 130.0000000000000000 ) ) ;
#3987=ORIENTED_EDGE ( 'NONE', *, *, #2213, .T. ) ;
#3988=EDGE_CURVE ( 'NONE', #511, #7515, #6407, .T. ) ;
#3990=VERTEX_POINT ( 'NONE', #2879 ) ;
#3992=ORIENTED_EDGE ( 'NONE', *, *, #7639, .T. ) ;
#3993=CYLINDRICAL_SURFACE ( 'NONE', #7914, 5.000000000000004441 ) ;
#3998=ORIENTED_EDGE ( 'NONE', *, *, #7243, .T. ) ;
#3999=CARTESIAN_POINT ( 'NONE',  ( 339.1025403784438481, 142.5000000000000000, 125.0000000000000000 ) ) ;
#4001=CARTESIAN_POINT ( 'NONE',  ( 296.6025403784437913, 142.5000000000000000, 155.0000000000000000 ) ) ;
#4004=DIRECTION ( 'NONE',  ( 0.000000000000000000, 0.000000000000000000, 1.000000000000000000 ) ) ;
#4007=ORIENTED_EDGE ( 'NONE', *, *, #3327, .F. ) ;
#4010=DIRECTION ( 'NONE',  ( 0.000000000000000000, 0.000000000000000000, 1.000000000000000000 ) ) ;
#4013=CARTESIAN_POINT ( 'NONE',  ( 200.0000000000000000, 0.000000000000000000, 12.50000000000000000 ) ) ;
#4021=CARTESIAN_POINT ( 'NONE',  ( -37.49999999999994316, 225.0000000000000284, 12.50000000000000000 ) ) ;
#4024=CIRCLE ( 'NONE', #2244, 37.50000000000000711 ) ;
#4025=ORIENTED_EDGE ( 'NONE', *, *, #4924, .T. ) ;
#4027=ORIENTED_EDGE ( 'NONE', *, *, #1491, .T. ) ;
#4028=AXIS2_PLACEMENT_3D ( 'NONE', #3961, #6327, #2154 ) ;
#4030=VECTOR ( 'NONE', #4261, 1000.000000000000000 ) ;
#4031=ORIENTED_EDGE ( 'NONE', *, *, #7893, .F. ) ;
#4033=ORIENTED_EDGE ( 'NONE', *, *, #4550, .T. ) ;
#4036=VERTEX_POINT ( 'NONE', #4148 ) ;
#4038=CARTESIAN_POINT ( 'NONE',  ( 212.5000000000000284, 1.530808498934191916E-15, 12.50000000000000000 ) ) ;
#4040=DIRECTION ( 'NONE',  ( 0.000000000000000000, 0.000000000000000000, 1.000000000000000000 ) ) ;
#4042=DIRECTION ( 'NONE',  ( -4.789677997474686366E-16, -1.000000000000000000, -0.000000000000000000 ) ) ;
#4043=AXIS2_PLACEMENT_3D ( 'NONE', #4084, #3492, #7651 ) ;
#4044=ORIENTED_EDGE ( 'NONE', *, *, #5227, .F. ) ;
#4046=EDGE_CURVE ( 'NONE', #5244, #2838, #471, .T. ) ;
#4052=ORIENTED_EDGE ( 'NONE', *, *, #72, .F. ) ;
#4053=EDGE_CURVE ( 'NONE', #7523, #4616, #630, .T. ) ;
#4054=CARTESIAN_POINT ( 'NONE',  ( 0.000000000000000000, -37.50000000000000000, 12.50000000000000000 ) ) ;
#4055=CARTESIAN_POINT ( 'NONE',  ( -37.49999999999989342, 177.4999999999999432, 5.000000000000000000 ) ) ;
#4057=DIRECTION ( 'NONE',  ( 0.000000000000000000, -8.474984920802721991E-16, 1.000000000000000000 ) ) ;
#4058=DIRECTION ( 'NONE',  ( 1.000000000000000000, 0.000000000000000000, 0.000000000000000000 ) ) ;
#4061=DIRECTION ( 'NONE',  ( -0.000000000000000000, -0.000000000000000000, -1.000000000000000000 ) ) ;
#4069=EDGE_LOOP ( 'NONE', ( #2805, #3848, #2837, #2603, #2912 ) ) ;
#4084=CARTESIAN_POINT ( 'NONE',  ( 0.000000000000000000, 0.000000000000000000, 0.000000000000000000 ) ) ;
#4085=AXIS2_PLACEMENT_3D ( 'NONE', #769, #287, #1487 ) ;
#4088=CARTESIAN_POINT ( 'NONE',  ( 52.50000000000000711, 47.50000000000003553, 12.50000000000000000 ) ) ;
#4092=EDGE_CURVE ( 'NONE', #642, #7501, #3542, .T. ) ;
#4095=CARTESIAN_POINT ( 'NONE',  ( 47.50000000000000711, 47.50000000000003553, 0.000000000000000000 ) ) ;
#4106=ORIENTED_EDGE ( 'NONE', *, *, #4134, .F. ) ;
#4109=ORIENTED_EDGE ( 'NONE', *, *, #724, .F. ) ;
#4110=CARTESIAN_POINT ( 'NONE',  ( 0.000000000000000000, 0.000000000000000000, 0.000000000000000000 ) ) ;
#4121=ORIENTED_EDGE ( 'NONE', *, *, #7065, .T. ) ;
#4126=VERTEX_POINT ( 'NONE', #1184 ) ;
#4127=ORIENTED_EDGE ( 'NONE', *, *, #3988, .F. ) ;
#4130=CARTESIAN_POINT ( 'NONE',  ( -6.945033096338293890E-14, 144.9999999999998295, 0.000000000000000000 ) ) ;
#4134=EDGE_CURVE ( 'NONE', #393, #7515, #5193, .T. ) ;
#4136=CARTESIAN_POINT ( 'NONE',  ( -12.49999999999996803, 225.0000000000000284, 0.000000000000000000 ) ) ;
#4141=CARTESIAN_POINT ( 'NONE',  ( 314.1025403784437344, 82.50000000000004263, 125.0000000000000000 ) ) ;
#4142=ORIENTED_EDGE ( 'NONE', *, *, #6320, .T. ) ;
#4143=EDGE_CURVE ( 'NONE', #5638, #1872, #5464, .T. ) ;
#4148=CARTESIAN_POINT ( 'NONE',  ( 42.50000000000000711, 187.5000000000000000, 12.50000000000000000 ) ) ;
#4150=DIRECTION ( 'NONE',  ( -1.000000000000000000, 0.000000000000000000, 0.000000000000000000 ) ) ;
#4151=AXIS2_PLACEMENT_3D ( 'NONE', #4660, #4546, #7763 ) ;
#4152=VECTOR ( 'NONE', #3627, 1000.000000000000000 ) ;
#4155=AXIS2_PLACEMENT_3D ( 'NONE', #2684, #2802, #5240 ) ;
#4158=FACE_OUTER_BOUND ( 'NONE', #3135, .T. ) ;
#4159=ORIENTED_EDGE ( 'NONE', *, *, #5576, .F. ) ;
#4161=ORIENTED_EDGE ( 'NONE', *, *, #1897, .F. ) ;
#4164=LINE ( 'NONE', #3572, #5444 ) ;
#4166=ORIENTED_EDGE ( 'NONE', *, *, #7702, .F. ) ;
#4168=ORIENTED_EDGE ( 'NONE', *, *, #311, .F. ) ;
#4172=CARTESIAN_POINT ( 'NONE',  ( 412.5000000000000568, 150.0000000000000284, 20.00000000000000000 ) ) ;
#4183=EDGE_LOOP ( 'NONE', ( #4958, #2367 ) ) ;
#4186=DIRECTION ( 'NONE',  ( 0.000000000000000000, 0.000000000000000000, 1.000000000000000000 ) ) ;
#4190=CIRCLE ( 'NONE', #7407, 12.50000000000000000 ) ;
#4193=ORIENTED_EDGE ( 'NONE', *, *, #7721, .F. ) ;
#4194=CARTESIAN_POINT ( 'NONE',  ( 41.25000000000002842, 47.50000000000003553, 17.50000000000000000 ) ) ;
#4195=AXIS2_PLACEMENT_3D ( 'NONE', #6942, #6263, #2692 ) ;
#4196=VECTOR ( 'NONE', #4465, 1000.000000000000000 ) ;
#4198=ORIENTED_EDGE ( 'NONE', *, *, #4457, .F. ) ;
#4199=CARTESIAN_POINT ( 'NONE',  ( 279.9038105676658006, 161.6025403784438765, 12.50000000000000000 ) ) ;
#4200=ORIENTED_EDGE ( 'NONE', *, *, #2206, .F. ) ;
#4203=CARTESIAN_POINT ( 'NONE',  ( -37.50000000000000000, 4.592427351555481498E-15, 12.50000000000000000 ) ) ;
#4204=AXIS2_PLACEMENT_3D ( 'NONE', #7436, #89, #7907 ) ;
#4214=CARTESIAN_POINT ( 'NONE',  ( 279.9038105676658006, 161.6025403784438765, 12.50000000000000000 ) ) ;
#4215=DIRECTION ( 'NONE',  ( -0.000000000000000000, -0.000000000000000000, -1.000000000000000000 ) ) ;
#4217=LINE ( 'NONE', #6669, #1347 ) ;
#4219=DIRECTION ( 'NONE',  ( -4.789677997474686366E-16, -1.000000000000000000, -0.000000000000000000 ) ) ;
#4221=DIRECTION ( 'NONE',  ( -4.789677997474686366E-16, -1.000000000000000000, 0.000000000000000000 ) ) ;
#4229=CARTESIAN_POINT ( 'NONE',  ( 314.1025403784437344, 75.00000000000005684, 125.0000000000000000 ) ) ;
#4232=ORIENTED_EDGE ( 'NONE', *, *, #4704, .T. ) ;
#4239=EDGE_LOOP ( 'NONE', ( #902, #7572, #4052, #7592, #6079, #6172 ) ) ;
#4245=EDGE_CURVE ( 'NONE', #5178, #3850, #6620, .T. ) ;
#4246=VERTEX_POINT ( 'NONE', #4511 ) ;
#4248=ORIENTED_EDGE ( 'NONE', *, *, #7721, .T. ) ;
#4251=ADVANCED_FACE ( 'NONE', ( #7558 ), #4504, .F. ) ;
#4252=CARTESIAN_POINT ( 'NONE',  ( 41.25000000000002842, 177.6587708172407076, 12.50000000000000000 ) ) ;
#4257=DIRECTION ( 'NONE',  ( 1.000000000000000000, 9.251858538542979716E-16, 0.000000000000000000 ) ) ;
#4258=PLANE ( 'NONE',  #4456 ) ;
#4261=DIRECTION ( 'NONE',  ( -1.000000000000000000, 4.789677997474686366E-16, -0.000000000000000000 ) ) ;
#4262=EDGE_CURVE ( 'NONE', #2065, #1547, #5221, .T. ) ;
#4269=AXIS2_PLACEMENT_3D ( 'NONE', #2864, #5256, #4058 ) ;
#4282=VECTOR ( 'NONE', #5935, 1000.000000000000000 ) ;
#4287=AXIS2_PLACEMENT_3D ( 'NONE', #1044, #6855, #3096 ) ;
#4298=FACE_OUTER_BOUND ( 'NONE', #6783, .T. ) ;
#4303=AXIS2_PLACEMENT_3D ( 'NONE', #4786, #3633, #3556 ) ;
#4307=DIRECTION ( 'NONE',  ( -4.789677997474686366E-16, -1.000000000000000000, 0.000000000000000000 ) ) ;
#4311=ORIENTED_EDGE ( 'NONE', *, *, #1211, .T. ) ;
#4313=DIRECTION ( 'NONE',  ( -1.000000000000000000, 0.000000000000000000, 0.000000000000000000 ) ) ;
#4316=VERTEX_POINT ( 'NONE', #7593 ) ;
#4318=ORIENTED_EDGE ( 'NONE', *, *, #5774, .T. ) ;
#4322=ORIENTED_EDGE ( 'NONE', *, *, #4053, .F. ) ;
#4325=DIRECTION ( 'NONE',  ( -0.000000000000000000, -0.000000000000000000, -1.000000000000000000 ) ) ;
#4328=CARTESIAN_POINT ( 'NONE',  ( 0.000000000000000000, 47.50000000000009237, 0.000000000000000000 ) ) ;
#4334=EDGE_CURVE ( 'NONE', #556, #2226, #2829, .T. ) ;
#4339=DIRECTION ( 'NONE',  ( 1.000000000000000000, 0.000000000000000000, 0.000000000000000000 ) ) ;
#4343=VERTEX_POINT ( 'NONE', #4581 ) ;
#4350=EDGE_CURVE ( 'NONE', #1859, #1477, #6365, .T. ) ;
#4351=CARTESIAN_POINT ( 'NONE',  ( 42.50000000000000711, 187.5000000000000000, 0.000000000000000000 ) ) ;
#4354=ORIENTED_EDGE ( 'NONE', *, *, #1207, .T. ) ;
#4355=DIRECTION ( 'NONE',  ( -1.000000000000000000, 0.000000000000000000, 0.000000000000000000 ) ) ;
#4361=MANIFOLD_SOLID_BREP ( 'Radyus3', #7351 ) ;
#4367=FACE_OUTER_BOUND ( 'NONE', #22, .T. ) ;
#4368=DIRECTION ( 'NONE',  ( -1.000000000000000000, 0.000000000000000000, 0.000000000000000000 ) ) ;
#4370=CARTESIAN_POINT ( 'NONE',  ( 412.4999999999998295, 145.0000000000000284, 0.000000000000000000 ) ) ;
#4371=CARTESIAN_POINT ( 'NONE',  ( 0.000000000000000000, 187.5000000000000000, 12.50000000000000000 ) ) ;
#4372=CARTESIAN_POINT ( 'NONE',  ( 46.25000000000002842, 144.7499999999999147, 130.0000000000000000 ) ) ;
#4373=DIRECTION ( 'NONE',  ( -1.000000000000000000, 0.000000000000000000, 0.000000000000000000 ) ) ;
#4378=CARTESIAN_POINT ( 'NONE',  ( 296.6025403784439050, 80.00000000000007105, 5.000000000000000000 ) ) ;
#4382=VERTEX_POINT ( 'NONE', #2913 ) ;
#4388=ORIENTED_EDGE ( 'NONE', *, *, #1283, .F. ) ;
#4391=ORIENTED_EDGE ( 'NONE', *, *, #6695, .F. ) ;
#4392=AXIS2_PLACEMENT_3D ( 'NONE', #1067, #5398, #433 ) ;
#4393=LINE ( 'NONE', #6250, #2817 ) ;
#4396=ORIENTED_EDGE ( 'NONE', *, *, #1834, .T. ) ;
#4401=EDGE_CURVE ( 'NONE', #4126, #1302, #1366, .T. ) ;
#4402=CARTESIAN_POINT ( 'NONE',  ( 187.5000000000000000, 0.000000000000000000, 12.50000000000000000 ) ) ;
#4403=CARTESIAN_POINT ( 'NONE',  ( 52.50000000000000711, 0.000000000000000000, 5.000000000000000000 ) ) ;
#4404=ORIENTED_EDGE ( 'NONE', *, *, #7404, .T. ) ;
#4405=AXIS2_PLACEMENT_3D ( 'NONE', #5521, #2061, #3233 ) ;
#4407=CARTESIAN_POINT ( 'NONE',  ( 0.000000000000000000, 177.4999999999999432, 0.000000000000000000 ) ) ;
#4411=CARTESIAN_POINT ( 'NONE',  ( 412.5000000000000568, 80.00000000000001421, 5.000000000000000000 ) ) ;
#4412=DIRECTION ( 'NONE',  ( 0.000000000000000000, -0.000000000000000000, -1.000000000000000000 ) ) ;
#4414=DIRECTION ( 'NONE',  ( -0.000000000000000000, -1.000000000000000000, -0.000000000000000000 ) ) ;
#4416=ORIENTED_EDGE ( 'NONE', *, *, #5562, .T. ) ;
#4417=DIRECTION ( 'NONE',  ( 1.000000000000000000, 4.789677997474691297E-16, 0.000000000000000000 ) ) ;
#4418=AXIS2_PLACEMENT_3D ( 'NONE', #1595, #4042, #6496 ) ;
#4421=DIRECTION ( 'NONE',  ( 2.960594732333750117E-15, -1.000000000000000000, 0.000000000000000000 ) ) ;
#4424=ORIENTED_EDGE ( 'NONE', *, *, #6661, .T. ) ;
#4428=EDGE_CURVE ( 'NONE', #30, #1382, #7277, .T. ) ;
#4433=VERTEX_POINT ( 'NONE', #6790 ) ;
#4441=ORIENTED_EDGE ( 'NONE', *, *, #385, .T. ) ;
#4443=LINE ( 'NONE', #4402, #617 ) ;
#4444=LINE ( 'NONE', #4403, #7548 ) ;
#4447=DIRECTION ( 'NONE',  ( -1.000000000000000000, 0.000000000000000000, 0.000000000000000000 ) ) ;
#4449=VECTOR ( 'NONE', #1118, 1000.000000000000000 ) ;
#4451=DIRECTION ( 'NONE',  ( -0.000000000000000000, 0.000000000000000000, 1.000000000000000000 ) ) ;
#4454=FACE_OUTER_BOUND ( 'NONE', #6300, .T. ) ;
#4456=AXIS2_PLACEMENT_3D ( 'NONE', #4371, #1370, #4412 ) ;
#4457=EDGE_CURVE ( 'NONE', #1583, #3990, #983, .T. ) ;
#4458=VERTEX_POINT ( 'NONE', #4370 ) ;
#4460=CIRCLE ( 'NONE', #1520, 65.50000000000000000 ) ;
#4465=DIRECTION ( 'NONE',  ( -1.295260195396012743E-15, -1.000000000000000000, 0.000000000000000000 ) ) ;
#4470=ORIENTED_EDGE ( 'NONE', *, *, #4980, .T. ) ;
#4471=CARTESIAN_POINT ( 'NONE',  ( -31.24999999999997158, 0.000000000000000000, 195.5000000000000000 ) ) ;
#4476=FACE_OUTER_BOUND ( 'NONE', #4069, .T. ) ;
#4477=CARTESIAN_POINT ( 'NONE',  ( -1.301042606982605321E-15, -37.50000000000000000, 0.000000000000000000 ) ) ;
#4479=EDGE_LOOP ( 'NONE', ( #77, #3647 ) ) ;
#4481=ORIENTED_EDGE ( 'NONE', *, *, #7893, .T. ) ;
#4482=EDGE_CURVE ( 'NONE', #3593, #3005, #5730, .T. ) ;
#4484=CARTESIAN_POINT ( 'NONE',  ( 42.50000000000000711, 182.5000000000000000, 0.000000000000000000 ) ) ;
#4498=LINE ( 'NONE', #4988, #936 ) ;
#4499=EDGE_CURVE ( 'NONE', #5649, #6617, #6369, .T. ) ;
#4504=CYLINDRICAL_SURFACE ( 'NONE', #7136, 12.49999999999999467 ) ;
#4505=CARTESIAN_POINT ( 'NONE',  ( 2.775557561562891351E-14, 225.0000000000000284, 0.000000000000000000 ) ) ;
#4506=DIRECTION ( 'NONE',  ( -1.295260195396012940E-15, 1.000000000000000000, 0.000000000000000000 ) ) ;
#4510=EDGE_LOOP ( 'NONE', ( #4847, #722, #1706, #266, #3872, #1286, #396 ) ) ;
#4511=CARTESIAN_POINT ( 'NONE',  ( -37.49999999999989342, 187.4999999999999432, 12.50000000000000000 ) ) ;
#4516=DIRECTION ( 'NONE',  ( 3.469446951953614189E-17, 1.000000000000000000, -0.000000000000000000 ) ) ;
#4517=AXIS2_PLACEMENT_3D ( 'NONE', #6702, #3662, #124 ) ;
#4522=EDGE_LOOP ( 'NONE', ( #5982, #7554 ) ) ;
#4523=DIRECTION ( 'NONE',  ( 1.295260195396013137E-15, -1.000000000000000000, 0.000000000000000000 ) ) ;
#4531=EDGE_CURVE ( 'NONE', #1859, #2637, #655, .T. ) ;
#4532=CIRCLE ( 'NONE', #2497, 32.75000000000000000 ) ;
#4533=AXIS2_PLACEMENT_3D ( 'NONE', #890, #3937, #3821 ) ;
#4540=VERTEX_POINT ( 'NONE', #3786 ) ;
#4542=ORIENTED_EDGE ( 'NONE', *, *, #3988, .T. ) ;
#4545=CYLINDRICAL_SURFACE ( 'NONE', #6331, 5.000000000000000888 ) ;
#4546=DIRECTION ( 'NONE',  ( 0.000000000000000000, -0.000000000000000000, -1.000000000000000000 ) ) ;
#4548=VECTOR ( 'NONE', #2678, 1000.000000000000000 ) ;
#4549=ORIENTED_EDGE ( 'NONE', *, *, #1322, .F. ) ;
#4550=EDGE_CURVE ( 'NONE', #1497, #2024, #3109, .T. ) ;
#4553=DIRECTION ( 'NONE',  ( 0.000000000000000000, 0.000000000000000000, -1.000000000000000000 ) ) ;
#4554=CARTESIAN_POINT ( 'NONE',  ( -27.08354679051374347, 177.4999999999999432, 12.55124306091976649 ) ) ;
#4557=FACE_OUTER_BOUND ( 'NONE', #7410, .T. ) ;
#4561=ORIENTED_EDGE ( 'NONE', *, *, #6000, .F. ) ;
#4568=CIRCLE ( 'NONE', #6887, 5.000000000000004441 ) ;
#4570=CARTESIAN_POINT ( 'NONE',  ( 187.5000000000000000, 0.000000000000000000, 12.50000000000000000 ) ) ;
#4571=DIRECTION ( 'NONE',  ( -0.000000000000000000, -0.000000000000000000, -1.000000000000000000 ) ) ;
#4572=CARTESIAN_POINT ( 'NONE',  ( 326.6025403784437913, 75.00000000000005684, 125.0000000000000000 ) ) ;
#4573=ADVANCED_FACE ( 'NONE', ( #3186 ), #6269, .F. ) ;
#4574=FACE_OUTER_BOUND ( 'NONE', #3754, .T. ) ;
#4576=AXIS2_PLACEMENT_3D ( 'NONE', #3947, #896, #6037 ) ;
#4579=ORIENTED_EDGE ( 'NONE', *, *, #862, .F. ) ;
#4581=CARTESIAN_POINT ( 'NONE',  ( -27.49999999999989342, 177.4999999999999432, 12.65877081724072362 ) ) ;
#4582=CARTESIAN_POINT ( 'NONE',  ( -37.49999999999995026, 47.50000000000009237, 12.50000000000000000 ) ) ;
#4584=DIRECTION ( 'NONE',  ( 1.000000000000000000, -4.789677997474686366E-16, -0.000000000000000000 ) ) ;
#4585=ADVANCED_FACE ( 'NONE', ( #2499 ), #3464, .F. ) ;
#4593=ORIENTED_EDGE ( 'NONE', *, *, #7360, .T. ) ;
#4596=DIRECTION ( 'NONE',  ( -1.000000000000000000, 0.000000000000000000, 0.000000000000000000 ) ) ;
#4598=LINE ( 'NONE', #4477, #2755 ) ;
#4600=FACE_OUTER_BOUND ( 'NONE', #3979, .T. ) ;
#4602=DIRECTION ( 'NONE',  ( -0.000000000000000000, -0.000000000000000000, -1.000000000000000000 ) ) ;
#4603=VERTEX_POINT ( 'NONE', #3935 ) ;
#4606=LINE ( 'NONE', #3458, #4449 ) ;
#4612=LINE ( 'NONE', #7070, #1327 ) ;
#4616=VERTEX_POINT ( 'NONE', #2695 ) ;
#4617=DIRECTION ( 'NONE',  ( 1.000000000000000000, 0.000000000000000000, 0.000000000000000000 ) ) ;
#4619=DIRECTION ( 'NONE',  ( 0.000000000000000000, 0.000000000000000000, 1.000000000000000000 ) ) ;
#4620=CARTESIAN_POINT ( 'NONE',  ( 326.6025403784438481, 150.0000000000000568, 125.0000000000000000 ) ) ;
#4626=DIRECTION ( 'NONE',  ( 1.000000000000000000, 0.000000000000000000, 0.000000000000000000 ) ) ;
#4628=DIRECTION ( 'NONE',  ( 0.000000000000000000, -0.000000000000000000, 1.000000000000000000 ) ) ;
#4629=CYLINDRICAL_SURFACE ( 'NONE', #6196, 5.000000000000004441 ) ;
#4635=ORIENTED_EDGE ( 'NONE', *, *, #6061, .T. ) ;
#4637=ORIENTED_EDGE ( 'NONE', *, *, #1181, .T. ) ;
#4638=LINE ( 'NONE', #4001, #4805 ) ;
#4647=LINE ( 'NONE', #1653, #6141 ) ;
#4648=CARTESIAN_POINT ( 'NONE',  ( -31.24999999999997158, 111.9999999999999289, 130.0000000000000000 ) ) ;
#4653=CIRCLE ( 'NONE', #4782, 32.75000000000000000 ) ;
#4660=CARTESIAN_POINT ( 'NONE',  ( -27.49999999999994671, 42.50000000000009237, 12.50000000000000000 ) ) ;
#4665=ORIENTED_EDGE ( 'NONE', *, *, #7805, .T. ) ;
#4667=CIRCLE ( 'NONE', #2609, 5.000000000000000000 ) ;
#4668=ORIENTED_EDGE ( 'NONE', *, *, #3809, .T. ) ;
#4673=DIRECTION ( 'NONE',  ( -0.000000000000000000, -0.000000000000000000, -1.000000000000000000 ) ) ;
#4678=CARTESIAN_POINT ( 'NONE',  ( 41.25000000000002842, 177.5000000000000000, 12.50000000000000000 ) ) ;
#4679=VERTEX_POINT ( 'NONE', #4054 ) ;
#4684=DIRECTION ( 'NONE',  ( -0.000000000000000000, -0.000000000000000000, -1.000000000000000000 ) ) ;
#4686=LINE ( 'NONE', #2975, #3144 ) ;
#4688=EDGE_LOOP ( 'NONE', ( #187, #472, #5272, #7824, #6497 ) ) ;
#4692=CARTESIAN_POINT ( 'NONE',  ( 0.000000000000000000, 111.9999999999999289, 130.0000000000000000 ) ) ;
#4695=CARTESIAN_POINT ( 'NONE',  ( 0.000000000000000000, 0.000000000000000000, 12.50000000000000000 ) ) ;
#4702=EDGE_LOOP ( 'NONE', ( #5492, #1953, #6334, #2062 ) ) ;
#4704=EDGE_CURVE ( 'NONE', #2195, #556, #2400, .T. ) ;
#4718=EDGE_LOOP ( 'NONE', ( #4870, #7417, #1782, #6473, #3216 ) ) ;
#4726=CARTESIAN_POINT ( 'NONE',  ( -37.50000000000000000, 4.592427351555481498E-15, 0.000000000000000000 ) ) ;
#4728=EDGE_CURVE ( 'NONE', #481, #6592, #5749, .T. ) ;
#4735=FACE_OUTER_BOUND ( 'NONE', #1972, .T. ) ;
#4737=EDGE_CURVE ( 'NONE', #5360, #698, #4766, .T. ) ;
#4739=CARTESIAN_POINT ( 'NONE',  ( 296.6025403784437913, 0.000000000000000000, 0.000000000000000000 ) ) ;
#4749=ORIENTED_EDGE ( 'NONE', *, *, #4499, .F. ) ;
#4754=VERTEX_POINT ( 'NONE', #4252 ) ;
#4758=DIRECTION ( 'NONE',  ( -0.000000000000000000, -0.000000000000000000, -1.000000000000000000 ) ) ;
#4763=DIRECTION ( 'NONE',  ( 0.000000000000000000, -0.000000000000000000, 1.000000000000000000 ) ) ;
#4764=ORIENTED_EDGE ( 'NONE', *, *, #1449, .T. ) ;
#4766=LINE ( 'NONE', #456, #4824 ) ;
#4769=LINE ( 'NONE', #6703, #6324 ) ;
#4775=AXIS2_PLACEMENT_3D ( 'NONE', #6941, #2081, #4004 ) ;
#4782=AXIS2_PLACEMENT_3D ( 'NONE', #3118, #6238, #5644 ) ;
#4785=VERTEX_POINT ( 'NONE', #571 ) ;
#4786=CARTESIAN_POINT ( 'NONE',  ( 412.5000000000000000, 87.50000000000005684, 17.49999999999998934 ) ) ;
#4790=ORIENTED_EDGE ( 'NONE', *, *, #1154, .F. ) ;
#4796=DIRECTION ( 'NONE',  ( -1.000000000000000000, 0.000000000000000000, -0.000000000000000000 ) ) ;
#4799=ORIENTED_EDGE ( 'NONE', *, *, #1283, .T. ) ;
#4801=VECTOR ( 'NONE', #7273, 1000.000000000000000 ) ;
#4805=VECTOR ( 'NONE', #4602, 1000.000000000000000 ) ;
#4814=CARTESIAN_POINT ( 'NONE',  ( 12.50000000000002309, 225.0000000000000284, 12.50000000000000000 ) ) ;
#4824=VECTOR ( 'NONE', #2902, 1000.000000000000000 ) ;
#4825=EDGE_LOOP ( 'NONE', ( #6537, #2709, #6460, #3728 ) ) ;
#4827=ORIENTED_EDGE ( 'NONE', *, *, #3123, .F. ) ;
#4830=DIRECTION ( 'NONE',  ( 1.000000000000000000, 0.000000000000000000, 0.000000000000000000 ) ) ;
#4831=AXIS2_PLACEMENT_3D ( 'NONE', #1202, #3703, #6144 ) ;
#4835=CARTESIAN_POINT ( 'NONE',  ( 199.9999999999998863, 262.5000000000000568, 12.50000000000000000 ) ) ;
#4836=CIRCLE ( 'NONE', #5997, 37.50000000000000711 ) ;
#4839=DIRECTION ( 'NONE',  ( 1.000000000000000000, 0.000000000000000000, 0.000000000000000000 ) ) ;
#4840=ORIENTED_EDGE ( 'NONE', *, *, #2793, .F. ) ;
#4844=DIRECTION ( 'NONE',  ( -0.000000000000000000, 0.000000000000000000, 1.000000000000000000 ) ) ;
#4846=DIRECTION ( 'NONE',  ( -0.000000000000000000, -0.000000000000000000, -1.000000000000000000 ) ) ;
#4847=ORIENTED_EDGE ( 'NONE', *, *, #2349, .T. ) ;
#4851=DIRECTION ( 'NONE',  ( -0.000000000000000000, 0.000000000000000000, 1.000000000000000000 ) ) ;
#4852=EDGE_CURVE ( 'NONE', #556, #5242, #3578, .T. ) ;
#4856=CARTESIAN_POINT ( 'NONE',  ( 62.50000000000008527, 111.9999999999998863, 130.0000000000000000 ) ) ;
#4857=CIRCLE ( 'NONE', #1397, 12.50000000000001066 ) ;
#4859=CARTESIAN_POINT ( 'NONE',  ( 326.6025403784437913, 149.9999999999999716, 125.0000000000000000 ) ) ;
#4862=CARTESIAN_POINT ( 'NONE',  ( 296.6025403784437913, 142.5000000000000000, 17.49999999999998934 ) ) ;
#4863=DIRECTION ( 'NONE',  ( 0.000000000000000000, -1.000000000000000000, 0.000000000000000000 ) ) ;
#4864=ORIENTED_EDGE ( 'NONE', *, *, #3585, .T. ) ;
#4865=ORIENTED_EDGE ( 'NONE', *, *, #3526, .T. ) ;
#4870=ORIENTED_EDGE ( 'NONE', *, *, #2435, .T. ) ;
#4872=PLANE ( 'NONE',  #6098 ) ;
#4875=EDGE_CURVE ( 'NONE', #4540, #2, #5583, .T. ) ;
#4880=LINE ( 'NONE', #6135, #2665 ) ;
#4885=ORIENTED_EDGE ( 'NONE', *, *, #6422, .T. ) ;
#4886=ORIENTED_EDGE ( 'NONE', *, *, #4401, .T. ) ;
#4888=CARTESIAN_POINT ( 'NONE',  ( 2.775557561562891351E-14, 262.5000000000000568, 12.50000000000000000 ) ) ;
#4890=CARTESIAN_POINT ( 'NONE',  ( 42.08354679051385006, 177.5000000000000000, 12.55124306091975761 ) ) ;
#4894=EDGE_CURVE ( 'NONE', #4382, #2195, #3814, .T. ) ;
#4897=( LENGTH_UNIT ( ) NAMED_UNIT ( * ) SI_UNIT ( .MILLI., .METRE. ) );
#4901=DIRECTION ( 'NONE',  ( 1.000000000000000000, 0.000000000000000000, 0.000000000000000000 ) ) ;
#4909=ORIENTED_EDGE ( 'NONE', *, *, #661, .F. ) ;
#4917=VERTEX_POINT ( 'NONE', #1288 ) ;
#4919=ORIENTED_EDGE ( 'NONE', *, *, #5175, .T. ) ;
#4920=EDGE_CURVE ( 'NONE', #6102, #2041, #4443, .T. ) ;
#4923=CIRCLE ( 'NONE', #4028, 12.50000000000001066 ) ;
#4924=EDGE_CURVE ( 'NONE', #6545, #2977, #5, .T. ) ;
#4931=CARTESIAN_POINT ( 'NONE',  ( -27.49999999999994671, 42.50000000000009237, 12.50000000000000000 ) ) ;
#4935=FACE_OUTER_BOUND ( 'NONE', #5274, .T. ) ;
#4938=DIRECTION ( 'NONE',  ( 0.000000000000000000, 0.000000000000000000, -1.000000000000000000 ) ) ;
#4939=DIRECTION ( 'NONE',  ( 1.000000000000000000, -1.387778780781445676E-15, 0.000000000000000000 ) ) ;
#4940=AXIS2_PLACEMENT_3D ( 'NONE', #7687, #4307, #6716 ) ;
#4950=EDGE_CURVE ( 'NONE', #279, #1497, #649, .T. ) ;
#4954=CARTESIAN_POINT ( 'NONE',  ( 314.1025403784437913, 150.0000000000000568, 125.0000000000000000 ) ) ;
#4958=ORIENTED_EDGE ( 'NONE', *, *, #6771, .F. ) ;
#4959=DIRECTION ( 'NONE',  ( 1.000000000000000000, -0.000000000000000000, 0.000000000000000000 ) ) ;
#4966=EDGE_CURVE ( 'NONE', #905, #2348, #5045, .T. ) ;
#4970=EDGE_LOOP ( 'NONE', ( #4885, #3528, #6453, #18 ) ) ;
#4975=CARTESIAN_POINT ( 'NONE',  ( -31.24999999999997158, 79.24999999999992895, 130.0000000000000000 ) ) ;
#4980=EDGE_CURVE ( 'NONE', #3684, #3773, #4568, .T. ) ;
#4983=AXIS2_PLACEMENT_3D ( 'NONE', #2324, #4758, #7217 ) ;
#4984=CARTESIAN_POINT ( 'NONE',  ( 296.6025403784439050, 87.50000000000005684, 17.49999999999998934 ) ) ;
#4986=CIRCLE ( 'NONE', #7807, 12.50000000000001066 ) ;
#4988=CARTESIAN_POINT ( 'NONE',  ( -26.24999999999997158, 0.000000000000000000, 12.50000000000000000 ) ) ;
#4992=ORIENTED_EDGE ( 'NONE', *, *, #2078, .F. ) ;
#4998=DIRECTION ( 'NONE',  ( 0.8948607650084221543, -4.286094916964204981E-16, 0.4463453945640545317 ) ) ;
#4999=EDGE_CURVE ( 'NONE', #5569, #5360, #4190, .T. ) ;
#5002=CARTESIAN_POINT ( 'NONE',  ( 46.25000000000002842, 177.5000000000000000, 195.5000000000000000 ) ) ;
#5003=ORIENTED_EDGE ( 'NONE', *, *, #3416, .F. ) ;
#5004=FACE_BOUND ( 'NONE', #230, .T. ) ;
#5005=DIRECTION ( 'NONE',  ( -0.000000000000000000, -0.000000000000000000, -1.000000000000000000 ) ) ;
#5006=VERTEX_POINT ( 'NONE', #2528 ) ;
#5009=LINE ( 'NONE', #7462, #5999 ) ;
#5010=CARTESIAN_POINT ( 'NONE',  ( -31.24999999999997158, 177.4999999999999432, 195.5000000000000000 ) ) ;
#5021=ORIENTED_EDGE ( 'NONE', *, *, #1154, .T. ) ;
#5024=CYLINDRICAL_SURFACE ( 'NONE', #1896, 5.000000000000004441 ) ;
#5025=LINE ( 'NONE', #7367, #6585 ) ;
#5027=LINE ( 'NONE', #7481, #951 ) ;
#5029=FACE_OUTER_BOUND ( 'NONE', #2298, .T. ) ;
#5034=VECTOR ( 'NONE', #2120, 1000.000000000000000 ) ;
#5039=ORIENTED_EDGE ( 'NONE', *, *, #2721, .T. ) ;
#5045=LINE ( 'NONE', #5010, #2408 ) ;
#5046=ORIENTED_EDGE ( 'NONE', *, *, #1501, .F. ) ;
#5049=DIRECTION ( 'NONE',  ( 4.789677997474698199E-16, -1.000000000000000000, 0.000000000000000000 ) ) ;
#5050=ADVANCED_FACE ( 'NONE', ( #5413 ), #6699, .T. ) ;
#5051=AXIS2_PLACEMENT_3D ( 'NONE', #7400, #6272, #4373 ) ;
#5055=CARTESIAN_POINT ( 'NONE',  ( 286.6025403784439050, 90.00000000000001421, 0.000000000000000000 ) ) ;
#5056=ADVANCED_FACE ( 'NONE', ( #648 ), #2490, .F. ) ;
#5058=CYLINDRICAL_SURFACE ( 'NONE', #2299, 5.000000000000000888 ) ;
#5059=ADVANCED_FACE ( 'NONE', ( #5699 ), #5156, .T. ) ;
#5065=FACE_OUTER_BOUND ( 'NONE', #5684, .T. ) ;
#5070=EDGE_LOOP ( 'NONE', ( #1797, #1427 ) ) ;
#5072=CARTESIAN_POINT ( 'NONE',  ( 37.50000000000000711, 42.50000000000003553, 0.000000000000000000 ) ) ;
#5081=VERTEX_POINT ( 'NONE', #6374 ) ;
#5082=CARTESIAN_POINT ( 'NONE',  ( 339.1025403784438481, 150.0000000000000568, 125.0000000000000000 ) ) ;
#5083=EDGE_LOOP ( 'NONE', ( #515, #5046, #761, #3574 ) ) ;
#5090=CYLINDRICAL_SURFACE ( 'NONE', #6329, 5.000000000000004441 ) ;
#5091=AXIS2_PLACEMENT_3D ( 'NONE', #361, #3411, #1642 ) ;
#5092=VECTOR ( 'NONE', #1736, 1000.000000000000000 ) ;
#5093=EDGE_CURVE ( 'NONE', #4679, #2900, #3247, .T. ) ;
#5097=CARTESIAN_POINT ( 'NONE',  ( 412.4999999999998863, 142.5000000000000000, 17.49999999999998934 ) ) ;
#5104=ORIENTED_EDGE ( 'NONE', *, *, #864, .T. ) ;
#5105=DIRECTION ( 'NONE',  ( -1.000000000000000000, -0.000000000000000000, 0.000000000000000000 ) ) ;
#5106=DIRECTION ( 'NONE',  ( -0.000000000000000000, -0.000000000000000000, -1.000000000000000000 ) ) ;
#5107=CARTESIAN_POINT ( 'NONE',  ( 412.5000000000000000, 87.50000000000005684, 12.50000000000000000 ) ) ;
#5109=ORIENTED_EDGE ( 'NONE', *, *, #1644, .F. ) ;
#5111=CARTESIAN_POINT ( 'NONE',  ( 314.1025403784437913, 150.0000000000000568, 125.0000000000000000 ) ) ;
#5114=DIRECTION ( 'NONE',  ( -1.000000000000000000, 0.000000000000000000, 0.000000000000000000 ) ) ;
#5121=ORIENTED_EDGE ( 'NONE', *, *, #1111, .T. ) ;
#5134=ORIENTED_EDGE ( 'NONE', *, *, #1177, .T. ) ;
#5136=EDGE_LOOP ( 'NONE', ( #6139, #3694, #2701, #2451 ) ) ;
#5140=DIRECTION ( 'NONE',  ( -1.000000000000000000, 4.270088556250607616E-16, -0.000000000000000000 ) ) ;
#5145=CARTESIAN_POINT ( 'NONE',  ( -32.49999999999997158, 1.387778780781446307E-14, 5.000000000000000000 ) ) ;
#5146=FACE_OUTER_BOUND ( 'NONE', #35, .T. ) ;
#5152=DIRECTION ( 'NONE',  ( 1.000000000000000000, -0.000000000000000000, -0.000000000000000000 ) ) ;
#5156=PLANE ( 'NONE',  #3056 ) ;
#5162=ORIENTED_EDGE ( 'NONE', *, *, #5475, .T. ) ;
#5163=EDGE_CURVE ( 'NONE', #477, #3284, #1373, .T. ) ;
#5171=DIRECTION ( 'NONE',  ( 1.000000000000000000, -0.000000000000000000, 0.000000000000000000 ) ) ;
#5172=VECTOR ( 'NONE', #1552, 1000.000000000000000 ) ;
#5174=CIRCLE ( 'NONE', #1602, 4.999999999999997335 ) ;
#5175=EDGE_CURVE ( 'NONE', #2269, #4603, #6260, .T. ) ;
#5178=VERTEX_POINT ( 'NONE', #6222 ) ;
#5181=AXIS2_PLACEMENT_3D ( 'NONE', #1345, #3798, #636 ) ;
#5183=FACE_BOUND ( 'NONE', #6930, .T. ) ;
#5185=EDGE_CURVE ( 'NONE', #6592, #2505, #5009, .T. ) ;
#5187=CARTESIAN_POINT ( 'NONE',  ( 326.6025403784438481, 142.5000000000000000, 125.0000000000000000 ) ) ;
#5188=ORIENTED_EDGE ( 'NONE', *, *, #4428, .T. ) ;
#5190=DIRECTION ( 'NONE',  ( 0.000000000000000000, 0.000000000000000000, 1.000000000000000000 ) ) ;
#5193=CIRCLE ( 'NONE', #4303, 5.000000000000004441 ) ;
#5198=ORIENTED_EDGE ( 'NONE', *, *, #5514, .T. ) ;
#5201=DIRECTION ( 'NONE',  ( -0.000000000000000000, 0.000000000000000000, 1.000000000000000000 ) ) ;
#5203=CARTESIAN_POINT ( 'NONE',  ( 296.6025403784437913, 149.9999999999999716, 5.000000000000000000 ) ) ;
#5211=DIRECTION ( 'NONE',  ( -4.605077885019035080E-16, -1.000000000000000000, 0.000000000000000000 ) ) ;
#5221=LINE ( 'NONE', #7118, #7778 ) ;
#5224=FACE_OUTER_BOUND ( 'NONE', #1072, .T. ) ;
#5226=ORIENTED_EDGE ( 'NONE', *, *, #6651, .T. ) ;
#5227=EDGE_CURVE ( 'NONE', #4036, #3284, #919, .T. ) ;
#5233=EDGE_LOOP ( 'NONE', ( #6319, #7723, #1511, #343, #5428, #2840, #53, #1794 ) ) ;
#5240=DIRECTION ( 'NONE',  ( 1.000000000000000000, -4.789677997474686366E-16, 0.000000000000000000 ) ) ;
#5242=VERTEX_POINT ( 'NONE', #3368 ) ;
#5244=VERTEX_POINT ( 'NONE', #4229 ) ;
#5248=DIRECTION ( 'NONE',  ( -4.789677997474686366E-16, -1.000000000000000000, -0.000000000000000000 ) ) ;
#5251=VERTEX_POINT ( 'NONE', #358 ) ;
#5253=CARTESIAN_POINT ( 'NONE',  ( 199.9999999999998863, 225.0000000000000284, 12.50000000000000000 ) ) ;
#5255=EDGE_CURVE ( 'NONE', #7842, #5551, #7647, .T. ) ;
#5256=DIRECTION ( 'NONE',  ( -0.000000000000000000, 0.000000000000000000, 1.000000000000000000 ) ) ;
#5264=DIRECTION ( 'NONE',  ( -0.000000000000000000, -0.000000000000000000, -1.000000000000000000 ) ) ;
#5267=VERTEX_POINT ( 'NONE', #3410 ) ;
#5272=ORIENTED_EDGE ( 'NONE', *, *, #946, .F. ) ;
#5273=ADVANCED_FACE ( 'NONE', ( #592 ), #2854, .T. ) ;
#5274=EDGE_LOOP ( 'NONE', ( #6043, #1596, #3433, #4391 ) ) ;
#5279=FACE_OUTER_BOUND ( 'NONE', #3732, .T. ) ;
#5281=ORIENTED_EDGE ( 'NONE', *, *, #2085, .F. ) ;
#5282=CARTESIAN_POINT ( 'NONE',  ( 46.25000000000002842, 79.24999999999990052, 130.0000000000000000 ) ) ;
#5286=DIRECTION ( 'NONE',  ( -0.000000000000000000, 0.000000000000000000, 1.000000000000000000 ) ) ;
#5288=CARTESIAN_POINT ( 'NONE',  ( -27.49999999999989342, 177.4999999999999432, 12.50000000000000000 ) ) ;
#5290=CARTESIAN_POINT ( 'NONE',  ( 200.0000000000000000, -37.50000000000000711, 12.50000000000000000 ) ) ;
#5292=EDGE_LOOP ( 'NONE', ( #6333, #257, #4992, #7057 ) ) ;
#5295=DIRECTION ( 'NONE',  ( 1.000000000000000000, 1.480297366166874072E-15, 0.000000000000000000 ) ) ;
#5296=FACE_OUTER_BOUND ( 'NONE', #6024, .T. ) ;
#5306=CARTESIAN_POINT ( 'NONE',  ( -31.24999999999997158, 47.50000000000009237, 130.0000000000000000 ) ) ;
#5307=FACE_BOUND ( 'NONE', #3826, .T. ) ;
#5311=VECTOR ( 'NONE', #657, 1000.000000000000000 ) ;
#5319=ORIENTED_EDGE ( 'NONE', *, *, #2213, .F. ) ;
#5332=PLANE ( 'NONE',  #1001 ) ;
#5334=EDGE_CURVE ( 'NONE', #6102, #2325, #99, .T. ) ;
#5346=AXIS2_PLACEMENT_3D ( 'NONE', #4984, #6229, #4938 ) ;
#5347=CARTESIAN_POINT ( 'NONE',  ( -37.49999999999997158, 1.601283208593976678E-14, 12.50000000000000000 ) ) ;
#5349=VERTEX_POINT ( 'NONE', #175 ) ;
#5360=VERTEX_POINT ( 'NONE', #7365 ) ;
#5363=ORIENTED_EDGE ( 'NONE', *, *, #5334, .T. ) ;
#5364=LINE ( 'NONE', #2967, #3908 ) ;
#5366=VECTOR ( 'NONE', #6521, 1000.000000000000000 ) ;
#5367=ORIENTED_EDGE ( 'NONE', *, *, #6747, .F. ) ;
#5368=CARTESIAN_POINT ( 'NONE',  ( 326.6025403784437913, 75.00000000000005684, 125.0000000000000000 ) ) ;
#5374=ADVANCED_FACE ( 'NONE', ( #5678 ), #5024, .F. ) ;
#5375=DIRECTION ( 'NONE',  ( 0.000000000000000000, 0.000000000000000000, -1.000000000000000000 ) ) ;
#5376=CARTESIAN_POINT ( 'NONE',  ( 0.000000000000000000, 262.5000000000000568, 12.50000000000000000 ) ) ;
#5377=ADVANCED_FACE ( 'NONE', ( #1938 ), #7479, .F. ) ;
#5380=EDGE_CURVE ( 'NONE', #4458, #3990, #7445, .T. ) ;
#5383=CARTESIAN_POINT ( 'NONE',  ( 296.6025403784437913, 137.4999999999999716, 17.49999999999998934 ) ) ;
#5384=CARTESIAN_POINT ( 'NONE',  ( 5.204170427930428856E-14, 37.50000000000005684, 0.000000000000000000 ) ) ;
#5386=DIRECTION ( 'NONE',  ( 1.000000000000000000, 0.000000000000000000, 0.000000000000000000 ) ) ;
#5389=DIRECTION ( 'NONE',  ( -1.000000000000000000, 0.000000000000000000, 0.000000000000000000 ) ) ;
#5398=DIRECTION ( 'NONE',  ( -4.789677997474686366E-16, -1.000000000000000000, -0.000000000000000000 ) ) ;
#5400=ORIENTED_EDGE ( 'NONE', *, *, #2775, .F. ) ;
#5401=DIRECTION ( 'NONE',  ( -0.000000000000000000, -0.000000000000000000, -1.000000000000000000 ) ) ;
#5403=LINE ( 'NONE', #2930, #117 ) ;
#5406=EDGE_LOOP ( 'NONE', ( #2664, #7768, #5400, #2399, #6435, #6530, #6907 ) ) ;
#5411=ORIENTED_EDGE ( 'NONE', *, *, #6750, .F. ) ;
#5413=FACE_OUTER_BOUND ( 'NONE', #3229, .T. ) ;
#5417=CARTESIAN_POINT ( 'NONE',  ( 412.4999999999998295, 145.0000000000000284, 5.000000000000000000 ) ) ;
#5418=CARTESIAN_POINT ( 'NONE',  ( 291.6025403784437913, 135.0000000000000000, 12.50000000000000000 ) ) ;
#5420=EDGE_CURVE ( 'NONE', #4679, #2146, #6237, .T. ) ;
#5421=CYLINDRICAL_SURFACE ( 'NONE', #1777, 12.50000000000001066 ) ;
#5422=AXIS2_PLACEMENT_3D ( 'NONE', #6039, #3549, #1219 ) ;
#5428=ORIENTED_EDGE ( 'NONE', *, *, #5807, .T. ) ;
#5434=( LENGTH_UNIT ( ) NAMED_UNIT ( * ) SI_UNIT ( .MILLI., .METRE. ) );
#5440=AXIS2_PLACEMENT_3D ( 'NONE', #3950, #981, #7167 ) ;
#5444=VECTOR ( 'NONE', #7853, 1000.000000000000000 ) ;
#5445=CIRCLE ( 'NONE', #1981, 5.000000000000000000 ) ;
#5446=ORIENTED_EDGE ( 'NONE', *, *, #7726, .F. ) ;
#5449=CARTESIAN_POINT ( 'NONE',  ( 412.4999999999998863, 142.5000000000000000, 155.0000000000000000 ) ) ;
#5453=DIRECTION ( 'NONE',  ( -0.000000000000000000, -0.000000000000000000, -1.000000000000000000 ) ) ;
#5454=CIRCLE ( 'NONE', #2378, 5.000000000000000000 ) ;
#5457=AXIS2_PLACEMENT_3D ( 'NONE', #7604, #7769, #4553 ) ;
#5463=DIRECTION ( 'NONE',  ( 0.000000000000000000, 0.000000000000000000, -1.000000000000000000 ) ) ;
#5464=CIRCLE ( 'NONE', #3677, 12.50000000000001066 ) ;
#5466=DIRECTION ( 'NONE',  ( 1.000000000000000000, 0.000000000000000000, 0.000000000000000000 ) ) ;
#5469=DIRECTION ( 'NONE',  ( -0.000000000000000000, -0.000000000000000000, -1.000000000000000000 ) ) ;
#5472=DIRECTION ( 'NONE',  ( 0.000000000000000000, 1.000000000000000000, 0.000000000000000000 ) ) ;
#5473=EDGE_CURVE ( 'NONE', #994, #4917, #362, .T. ) ;
#5475=EDGE_CURVE ( 'NONE', #5267, #5496, #7406, .T. ) ;
#5476=ORIENTED_EDGE ( 'NONE', *, *, #2823, .F. ) ;
#5478=VERTEX_POINT ( 'NONE', #6162 ) ;
#5482=DIRECTION ( 'NONE',  ( -4.789677997474686366E-16, -1.000000000000000000, -0.000000000000000000 ) ) ;
#5485=DIRECTION ( 'NONE',  ( 4.237492460401360996E-16, 1.000000000000000000, -8.474984920802721991E-16 ) ) ;
#5486=AXIS2_PLACEMENT_3D ( 'NONE', #3291, #5782, #5375 ) ;
#5487=VECTOR ( 'NONE', #140, 1000.000000000000000 ) ;
#5489=LINE ( 'NONE', #6052, #6016 ) ;
#5492=ORIENTED_EDGE ( 'NONE', *, *, #2293, .F. ) ;
#5494=DIRECTION ( 'NONE',  ( -1.000000000000000000, 4.270088556250607616E-16, -0.000000000000000000 ) ) ;
#5496=VERTEX_POINT ( 'NONE', #1305 ) ;
#5497=AXIS2_PLACEMENT_3D ( 'NONE', #6705, #3668, #3108 ) ;
#5503=DIRECTION ( 'NONE',  ( 0.5000000000000001110, -0.8660254037844385966, 0.000000000000000000 ) ) ;
#5514=EDGE_CURVE ( 'NONE', #7523, #393, #5643, .T. ) ;
#5521=CARTESIAN_POINT ( 'NONE',  ( -31.24999999999997158, 111.9999999999999289, 130.0000000000000000 ) ) ;
#5524=FACE_OUTER_BOUND ( 'NONE', #7448, .T. ) ;
#5525=UNCERTAINTY_MEASURE_WITH_UNIT (LENGTH_MEASURE( 1.000000000000000082E-05 ), #5434, 'distance_accuracy_value', 'NONE');
#5531=ORIENTED_EDGE ( 'NONE', *, *, #2078, .T. ) ;
#5545=CARTESIAN_POINT ( 'NONE',  ( 286.6025403784439050, 90.00000000000001421, 12.50000000000000000 ) ) ;
#5548=DIRECTION ( 'NONE',  ( -0.000000000000000000, -0.000000000000000000, -1.000000000000000000 ) ) ;
#5551=VERTEX_POINT ( 'NONE', #978 ) ;
#5555=CARTESIAN_POINT ( 'NONE',  ( 200.0000000000000000, 0.000000000000000000, 0.000000000000000000 ) ) ;
#5556=ORIENTED_EDGE ( 'NONE', *, *, #6651, .F. ) ;
#5562=EDGE_CURVE ( 'NONE', #5860, #6805, #5876, .T. ) ;
#5563=VERTEX_POINT ( 'NONE', #6396 ) ;
#5566=VECTOR ( 'NONE', #5140, 1000.000000000000000 ) ;
#5567=ORIENTED_EDGE ( 'NONE', *, *, #4875, .T. ) ;
#5569=VERTEX_POINT ( 'NONE', #5835 ) ;
#5573=VECTOR ( 'NONE', #1429, 1000.000000000000000 ) ;
#5575=AXIS2_PLACEMENT_3D ( 'NONE', #5383, #1567, #4010 ) ;
#5576=EDGE_CURVE ( 'NONE', #1704, #2, #7911, .T. ) ;
#5581=CARTESIAN_POINT ( 'NONE',  ( -27.49999999999989342, 182.4999999999999432, 12.50000000000000000 ) ) ;
#5583=LINE ( 'NONE', #4888, #613 ) ;
#5586=FACE_OUTER_BOUND ( 'NONE', #4239, .T. ) ;
#5587=CARTESIAN_POINT ( 'NONE',  ( -31.24999999999997158, 177.4999999999999432, 17.50000000000001421 ) ) ;
#5595=EDGE_CURVE ( 'NONE', #2226, #1787, #7677, .T. ) ;
#5598=ORIENTED_EDGE ( 'NONE', *, *, #7439, .F. ) ;
#5609=CARTESIAN_POINT ( 'NONE',  ( 296.6025403784439050, 82.50000000000004263, 125.0000000000000000 ) ) ;
#5613=DIRECTION ( 'NONE',  ( -1.000000000000000000, 0.000000000000000000, 0.000000000000000000 ) ) ;
#5614=LINE ( 'NONE', #791, #2625 ) ;
#5618=ORIENTED_EDGE ( 'NONE', *, *, #3083, .T. ) ;
#5619=VECTOR ( 'NONE', #6631, 1000.000000000000000 ) ;
#5621=VECTOR ( 'NONE', #1852, 1000.000000000000000 ) ;
#5624=DIRECTION ( 'NONE',  ( -0.000000000000000000, -0.000000000000000000, -1.000000000000000000 ) ) ;
#5626=DIRECTION ( 'NONE',  ( -4.789677997474686366E-16, -1.000000000000000000, -0.000000000000000000 ) ) ;
#5627=EDGE_CURVE ( 'NONE', #161, #1161, #7517, .T. ) ;
#5628=DIRECTION ( 'NONE',  ( 0.000000000000000000, 0.000000000000000000, 1.000000000000000000 ) ) ;
#5629=AXIS2_PLACEMENT_3D ( 'NONE', #6332, #397, #2687 ) ;
#5638=VERTEX_POINT ( 'NONE', #2098 ) ;
#5643=LINE ( 'NONE', #857, #5746 ) ;
#5644=DIRECTION ( 'NONE',  ( -4.237492460401360996E-16, -1.000000000000000000, 0.000000000000000000 ) ) ;
#5647=DIRECTION ( 'NONE',  ( -1.000000000000000000, 4.270088556250607616E-16, -0.000000000000000000 ) ) ;
#5649=VERTEX_POINT ( 'NONE', #6432 ) ;
#5650=EDGE_CURVE ( 'NONE', #3493, #1999, #933, .T. ) ;
#5657=ORIENTED_EDGE ( 'NONE', *, *, #4924, .F. ) ;
#5659=CARTESIAN_POINT ( 'NONE',  ( 333.3156402192583414, 150.0000000000000000, 178.7536863448640929 ) ) ;
#5666=CARTESIAN_POINT ( 'NONE',  ( 326.6025403784438481, 150.0000000000000568, 125.0000000000000000 ) ) ;
#5668=CARTESIAN_POINT ( 'NONE',  ( -31.24999999999997158, 177.4999999999999432, 130.0000000000000000 ) ) ;
#5670=EDGE_CURVE ( 'NONE', #2126, #7160, #3563, .T. ) ;
#5671=EDGE_CURVE ( 'NONE', #5242, #2348, #7836, .T. ) ;
#5672=ORIENTED_EDGE ( 'NONE', *, *, #1795, .T. ) ;
#5678=FACE_OUTER_BOUND ( 'NONE', #3530, .T. ) ;
#5684=EDGE_LOOP ( 'NONE', ( #5319, #4200, #645, #5039 ) ) ;
#5688=AXIS2_PLACEMENT_3D ( 'NONE', #1969, #5548, #1413 ) ;
#5690=VECTOR ( 'NONE', #1705, 1000.000000000000000 ) ;
#5696=LINE ( 'NONE', #2645, #7547 ) ;
#5697=ORIENTED_EDGE ( 'NONE', *, *, #4894, .T. ) ;
#5698=EDGE_LOOP ( 'NONE', ( #1624, #3087 ) ) ;
#5699=FACE_OUTER_BOUND ( 'NONE', #5903, .T. ) ;
#5703=AXIS2_PLACEMENT_3D ( 'NONE', #4620, #7717, #338 ) ;
#5707=AXIS2_PLACEMENT_3D ( 'NONE', #6583, #1690, #6465 ) ;
#5713=AXIS2_PLACEMENT_3D ( 'NONE', #3088, #6203, #6685 ) ;
#5714=ORIENTED_EDGE ( 'NONE', *, *, #3316, .F. ) ;
#5716=CIRCLE ( 'NONE', #4043, 12.50000000000000000 ) ;
#5718=ORIENTED_EDGE ( 'NONE', *, *, #5380, .F. ) ;
#5724=ORIENTED_EDGE ( 'NONE', *, *, #5671, .T. ) ;
#5726=ADVANCED_FACE ( 'NONE', ( #1137 ), #507, .T. ) ;
#5729=CARTESIAN_POINT ( 'NONE',  ( -27.49999999999989342, 187.4999999999999432, 12.50000000000000000 ) ) ;
#5730=CIRCLE ( 'NONE', #2519, 4.999999999999997335 ) ;
#5732=DIRECTION ( 'NONE',  ( -1.295260195396012743E-15, -1.000000000000000000, 0.000000000000000000 ) ) ;
#5735=VERTEX_POINT ( 'NONE', #2382 ) ;
#5736=DIRECTION ( 'NONE',  ( -1.000000000000000000, 0.000000000000000000, 0.000000000000000000 ) ) ;
#5738=ORIENTED_EDGE ( 'NONE', *, *, #5163, .T. ) ;
#5745=AXIS2_PLACEMENT_3D ( 'NONE', #69, #4844, #2521 ) ;
#5746=VECTOR ( 'NONE', #2746, 1000.000000000000000 ) ;
#5749=LINE ( 'NONE', #3374, #1885 ) ;
#5767=ORIENTED_EDGE ( 'NONE', *, *, #862, .T. ) ;
#5770=FACE_BOUND ( 'NONE', #4522, .T. ) ;
#5773=CARTESIAN_POINT ( 'NONE',  ( -1.301042606982605321E-15, -37.50000000000000000, 12.50000000000000000 ) ) ;
#5774=EDGE_CURVE ( 'NONE', #30, #3534, #1618, .T. ) ;
#5776=ORIENTED_EDGE ( 'NONE', *, *, #4092, .F. ) ;
#5781=LINE ( 'NONE', #2728, #2495 ) ;
#5782=DIRECTION ( 'NONE',  ( 0.000000000000000000, -1.000000000000000000, 0.000000000000000000 ) ) ;
#5785=AXIS2_PLACEMENT_3D ( 'NONE', #4110, #4186, #2351 ) ;
#5787=DIRECTION ( 'NONE',  ( -4.789677997474686366E-16, -1.000000000000000000, -0.000000000000000000 ) ) ;
#5791=CARTESIAN_POINT ( 'NONE',  ( -32.49999999999995026, 47.50000000000009237, 5.000000000000000000 ) ) ;
#5796=ORIENTED_EDGE ( 'NONE', *, *, #2157, .F. ) ;
#5799=DIRECTION ( 'NONE',  ( 1.295260195396012940E-15, 1.000000000000000000, 0.000000000000000000 ) ) ;
#5805=DIRECTION ( 'NONE',  ( -4.270088556250607616E-16, -1.000000000000000000, 0.000000000000000000 ) ) ;
#5806=CARTESIAN_POINT ( 'NONE',  ( -26.24999999999997158, 177.6587708172406224, 12.50000000000000000 ) ) ;
#5807=EDGE_CURVE ( 'NONE', #7780, #5649, #7800, .T. ) ;
#5808=LINE ( 'NONE', #7646, #1722 ) ;
#5809=ORIENTED_EDGE ( 'NONE', *, *, #724, .T. ) ;
#5813=DIRECTION ( 'NONE',  ( 0.5000000000000001110, 0.8660254037844385966, 0.000000000000000000 ) ) ;
#5821=ORIENTED_EDGE ( 'NONE', *, *, #3807, .T. ) ;
#5826=DIRECTION ( 'NONE',  ( -1.000000000000000000, 4.270088556250607616E-16, 0.000000000000000000 ) ) ;
#5827=CARTESIAN_POINT ( 'NONE',  ( -12.49999999999996803, 225.0000000000000284, 12.50000000000000000 ) ) ;
#5828=CARTESIAN_POINT ( 'NONE',  ( 0.000000000000000000, -37.50000000000000000, 0.000000000000000000 ) ) ;
#5835=CARTESIAN_POINT ( 'NONE',  ( 12.50000000000000000, 1.530808498934191521E-15, 12.50000000000000000 ) ) ;
#5836=AXIS2_PLACEMENT_3D ( 'NONE', #2438, #3200, #707 ) ;
#5837=DIRECTION ( 'NONE',  ( -1.000000000000000000, 0.000000000000000000, 0.000000000000000000 ) ) ;
#5839=CYLINDRICAL_SURFACE ( 'NONE', #5703, 12.50000000000001066 ) ;
#5840=ORIENTED_EDGE ( 'NONE', *, *, #2533, .T. ) ;
#5845=ORIENTED_EDGE ( 'NONE', *, *, #6750, .T. ) ;
#5849=FACE_BOUND ( 'NONE', #5890, .T. ) ;
#5850=ORIENTED_EDGE ( 'NONE', *, *, #765, .F. ) ;
#5851=VECTOR ( 'NONE', #5469, 1000.000000000000000 ) ;
#5852=CARTESIAN_POINT ( 'NONE',  ( 0.000000000000000000, 0.000000000000000000, 0.000000000000000000 ) ) ;
#5854=LINE ( 'NONE', #3366, #1355 ) ;
#5860=VERTEX_POINT ( 'NONE', #2500 ) ;
#5863=DIRECTION ( 'NONE',  ( 0.000000000000000000, 1.000000000000000000, 0.000000000000000000 ) ) ;
#5866=LINE ( 'NONE', #2091, #6966 ) ;
#5870=EDGE_CURVE ( 'NONE', #2527, #6578, #1930, .T. ) ;
#5876=LINE ( 'NONE', #1541, #4196 ) ;
#5879=FACE_OUTER_BOUND ( 'NONE', #7131, .T. ) ;
#5880=EDGE_LOOP ( 'NONE', ( #1104, #34, #6952, #170 ) ) ;
#5887=DIRECTION ( 'NONE',  ( -0.000000000000000000, -0.000000000000000000, -1.000000000000000000 ) ) ;
#5890=EDGE_LOOP ( 'NONE', ( #5446, #3512 ) ) ;
#5891=FACE_OUTER_BOUND ( 'NONE', #4510, .T. ) ;
#5893=ADVANCED_FACE ( 'NONE', ( #7318 ), #4258, .T. ) ;
#5894=DIRECTION ( 'NONE',  ( -1.000000000000000000, 0.000000000000000000, 0.000000000000000000 ) ) ;
#5895=ORIENTED_EDGE ( 'NONE', *, *, #4143, .T. ) ;
#5896=CARTESIAN_POINT ( 'NONE',  ( 199.9999999999998863, 225.0000000000000284, 0.000000000000000000 ) ) ;
#5897=ORIENTED_EDGE ( 'NONE', *, *, #4053, .T. ) ;
#5903=EDGE_LOOP ( 'NONE', ( #4109, #6382, #660, #4441 ) ) ;
#5909=DIRECTION ( 'NONE',  ( 0.000000000000000000, 0.000000000000000000, 1.000000000000000000 ) ) ;
#5912=LINE ( 'NONE', #4739, #5619 ) ;
#5913=ORIENTED_EDGE ( 'NONE', *, *, #4950, .T. ) ;
#5919=ADVANCED_FACE ( 'NONE', ( #4298 ), #3149, .F. ) ;
#5923=EDGE_CURVE ( 'NONE', #5860, #6773, #1893, .T. ) ;
#5934=DIRECTION ( 'NONE',  ( -0.000000000000000000, 0.000000000000000000, 1.000000000000000000 ) ) ;
#5935=DIRECTION ( 'NONE',  ( -0.000000000000000000, -0.000000000000000000, -1.000000000000000000 ) ) ;
#5944=CIRCLE ( 'NONE', #3514, 12.50000000000001066 ) ;
#5946=CARTESIAN_POINT ( 'NONE',  ( -31.24999999999997158, 112.5000000000000142, 195.4980915752512658 ) ) ;
#5948=VECTOR ( 'NONE', #6619, 1000.000000000000000 ) ;
#5954=CARTESIAN_POINT ( 'NONE',  ( 296.6025403784437913, 82.50000000000004263, 155.0000000000000000 ) ) ;
#5956=DIRECTION ( 'NONE',  ( -0.000000000000000000, 0.000000000000000000, 1.000000000000000000 ) ) ;
#5963=AXIS2_PLACEMENT_3D ( 'NONE', #4013, #1611, #7155 ) ;
#5964=( NAMED_UNIT ( * ) PLANE_ANGLE_UNIT ( ) SI_UNIT ( $, .RADIAN. ) );
#5966=CARTESIAN_POINT ( 'NONE',  ( 296.6025403784437913, 142.5000000000000000, 155.0000000000000000 ) ) ;
#5967=B_SPLINE_CURVE_WITH_KNOTS ( 'NONE', 3,
 ( #302, #2760, #7644, #2152 ),
 .UNSPECIFIED., .F., .F.,
 ( 4, 4 ),
 ( 0.000000000000000000, 0.001270006434950037748 ),
 .UNSPECIFIED. ) ;
#5968=CYLINDRICAL_SURFACE ( 'NONE', #4392, 29.99999999999997158 ) ;
#5974=DIRECTION ( 'NONE',  ( -0.5000000000000002220, 0.8660254037844384856, 0.000000000000000000 ) ) ;
#5976=DIRECTION ( 'NONE',  ( 0.000000000000000000, -0.000000000000000000, -1.000000000000000000 ) ) ;
#5982=ORIENTED_EDGE ( 'NONE', *, *, #7821, .T. ) ;
#5985=CARTESIAN_POINT ( 'NONE',  ( 326.6025403784437913, 82.50000000000004263, 125.0000000000000000 ) ) ;
#5987=CARTESIAN_POINT ( 'NONE',  ( 2.775557561562891351E-14, 225.0000000000000284, 12.50000000000000000 ) ) ;
#5991=DIRECTION ( 'NONE',  ( 1.000000000000000000, -4.270088556250607616E-16, 0.000000000000000000 ) ) ;
#5996=CARTESIAN_POINT ( 'NONE',  ( 296.6025403784439050, 80.00000000000007105, 0.000000000000000000 ) ) ;
#5997=AXIS2_PLACEMENT_3D ( 'NONE', #2895, #5934, #7221 ) ;
#5999=VECTOR ( 'NONE', #6297, 1000.000000000000000 ) ;
#6000=EDGE_CURVE ( 'NONE', #6519, #7538, #7033, .T. ) ;
#6001=ORIENTED_EDGE ( 'NONE', *, *, #2988, .T. ) ;
#6002=AXIS2_PLACEMENT_3D ( 'NONE', #7493, #2112, #870 ) ;
#6004=EDGE_LOOP ( 'NONE', ( #4159, #1531, #7329, #5567 ) ) ;
#6005=CARTESIAN_POINT ( 'NONE',  ( 326.6025403784437913, 82.50000000000004263, 125.0000000000000000 ) ) ;
#6006=CARTESIAN_POINT ( 'NONE',  ( -32.49999999999995026, 47.50000000000009237, 0.000000000000000000 ) ) ;
#6009=CIRCLE ( 'NONE', #3073, 5.000000000000000000 ) ;
#6012=EDGE_CURVE ( 'NONE', #2876, #1544, #1009, .T. ) ;
#6013=ORIENTED_EDGE ( 'NONE', *, *, #2293, .T. ) ;
#6015=EDGE_LOOP ( 'NONE', ( #786, #1046, #4799, #3287, #4637 ) ) ;
#6016=VECTOR ( 'NONE', #1636, 1000.000000000000000 ) ;
#6021=EDGE_CURVE ( 'NONE', #4246, #5251, #325, .T. ) ;
#6024=EDGE_LOOP ( 'NONE', ( #1085, #7574, #4007, #5697 ) ) ;
#6037=DIRECTION ( 'NONE',  ( 1.000000000000000000, 0.000000000000000000, 0.000000000000000000 ) ) ;
#6039=CARTESIAN_POINT ( 'NONE',  ( 199.9999999999998863, 225.0000000000000284, 12.50000000000000000 ) ) ;
#6040=ORIENTED_EDGE ( 'NONE', *, *, #6839, .T. ) ;
#6043=ORIENTED_EDGE ( 'NONE', *, *, #2255, .F. ) ;
#6052=CARTESIAN_POINT ( 'NONE',  ( 335.4891275541129971, 82.50000000000004263, 174.3961449365926626 ) ) ;
#6060=VECTOR ( 'NONE', #5626, 1000.000000000000000 ) ;
#6061=EDGE_CURVE ( 'NONE', #5349, #4036, #2419, .T. ) ;
#6065=CARTESIAN_POINT ( 'NONE',  ( -26.24999999999997158, 0.000000000000000000, 17.50000000000001421 ) ) ;
#6067=DIRECTION ( 'NONE',  ( -0.000000000000000000, -0.000000000000000000, -1.000000000000000000 ) ) ;
#6072=CARTESIAN_POINT ( 'NONE',  ( 286.6025403784437913, 150.0000000000000284, 12.50000000000000000 ) ) ;
#6075=LINE ( 'NONE', #6155, #1723 ) ;
#6077=AXIS2_PLACEMENT_3D ( 'NONE', #5417, #7350, #7902 ) ;
#6078=VECTOR ( 'NONE', #4584, 1000.000000000000000 ) ;
#6079=ORIENTED_EDGE ( 'NONE', *, *, #5671, .F. ) ;
#6088=VERTEX_POINT ( 'NONE', #2129 ) ;
#6089=DIRECTION ( 'NONE',  ( 0.4463453945640545317, 0.000000000000000000, -0.8948607650084221543 ) ) ;
#6090=CIRCLE ( 'NONE', #3272, 5.000000000000004441 ) ;
#6091=ORIENTED_EDGE ( 'NONE', *, *, #5923, .F. ) ;
#6098=AXIS2_PLACEMENT_3D ( 'NONE', #1826, #4998, #6089 ) ;
#6102=VERTEX_POINT ( 'NONE', #4570 ) ;
#6105=DIRECTION ( 'NONE',  ( 0.5000000000000001110, -0.8660254037844385966, 0.000000000000000000 ) ) ;
#6106=CYLINDRICAL_SURFACE ( 'NONE', #3122, 5.000000000000000888 ) ;
#6110=ADVANCED_FACE ( 'NONE', ( #3861 ), #7068, .F. ) ;
#6113=( GEOMETRIC_REPRESENTATION_CONTEXT ( 3 ) GLOBAL_UNCERTAINTY_ASSIGNED_CONTEXT ( ( #1506 ) ) GLOBAL_UNIT_ASSIGNED_CONTEXT ( ( #4897, #1663, #1698 ) ) REPRESENTATION_CONTEXT ( 'NONE', 'WORKASPACE' ) );
#6117=CYLINDRICAL_SURFACE ( 'NONE', #5422, 12.50000000000001066 ) ;
#6122=DIRECTION ( 'NONE',  ( -4.237492460401359023E-16, -1.000000000000000000, 0.000000000000000000 ) ) ;
#6123=AXIS2_PLACEMENT_3D ( 'NONE', #1788, #5201, #4830 ) ;
#6125=CARTESIAN_POINT ( 'NONE',  ( 286.6025403784439050, 90.00000000000001421, 12.50000000000000000 ) ) ;
#6131=ORIENTED_EDGE ( 'NONE', *, *, #4334, .F. ) ;
#6135=CARTESIAN_POINT ( 'NONE',  ( -27.49999999999994671, 47.50000000000009237, 12.50000000000000000 ) ) ;
#6139=ORIENTED_EDGE ( 'NONE', *, *, #7439, .T. ) ;
#6141=VECTOR ( 'NONE', #1607, 1000.000000000000000 ) ;
#6142=ORIENTED_EDGE ( 'NONE', *, *, #7821, .F. ) ;
#6144=DIRECTION ( 'NONE',  ( 0.4463453945640545317, 0.000000000000000000, -0.8948607650084221543 ) ) ;
#6148=CARTESIAN_POINT ( 'NONE',  ( 46.25000000000002842, 111.9999999999999858, 130.0000000000000000 ) ) ;
#6153=DIRECTION ( 'NONE',  ( 0.000000000000000000, 1.000000000000000000, 0.000000000000000000 ) ) ;
#6155=CARTESIAN_POINT ( 'NONE',  ( 212.4999999999999147, 225.0000000000000284, 12.50000000000000000 ) ) ;
#6156=ADVANCED_FACE ( 'NONE', ( #6270 ), #889, .F. ) ;
#6162=CARTESIAN_POINT ( 'NONE',  ( 232.4759526419164786, -18.74999999999998934, 12.50000000000000000 ) ) ;
#6167=DIRECTION ( 'NONE',  ( 0.000000000000000000, 0.000000000000000000, 1.000000000000000000 ) ) ;
#6171=PRODUCT_DEFINITION_FORMATION_WITH_SPECIFIED_SOURCE ( 'ANY', '', #1621, .NOT_KNOWN. ) ;
#6172=ORIENTED_EDGE ( 'NONE', *, *, #3921, .F. ) ;
#6186=CARTESIAN_POINT ( 'NONE',  ( -34.37499999999996447, 112.5000000000000142, 195.4980915752512658 ) ) ;
#6188=DIRECTION ( 'NONE',  ( 0.000000000000000000, 1.000000000000000000, 0.000000000000000000 ) ) ;
#6189=DIRECTION ( 'NONE',  ( -0.000000000000000000, -0.000000000000000000, -1.000000000000000000 ) ) ;
#6196=AXIS2_PLACEMENT_3D ( 'NONE', #989, #1549, #3400 ) ;
#6203=DIRECTION ( 'NONE',  ( 0.000000000000000000, -0.000000000000000000, -1.000000000000000000 ) ) ;
#6204=AXIS2_PLACEMENT_3D ( 'NONE', #337, #6317, #5799 ) ;
#6213=ORIENTED_EDGE ( 'NONE', *, *, #2793, .T. ) ;
#6215=AXIS2_PLACEMENT_3D ( 'NONE', #5376, #7822, #4763 ) ;
#6217=CIRCLE ( 'NONE', #5575, 5.000000000000000888 ) ;
#6219=EDGE_LOOP ( 'NONE', ( #5718, #6447, #7074, #3516, #2289, #5672, #5198, #6436, #4127, #3203, #143, #2193 ) ) ;
#6222=CARTESIAN_POINT ( 'NONE',  ( 296.6025403784439050, 80.00000000000007105, 0.000000000000000000 ) ) ;
#6224=CARTESIAN_POINT ( 'NONE',  ( -27.49999999999994671, 42.50000000000009237, 0.000000000000000000 ) ) ;
#6226=LINE ( 'NONE', #6788, #6588 ) ;
#6227=AXIS2_PLACEMENT_3D ( 'NONE', #7528, #4355, #6929 ) ;
#6229=DIRECTION ( 'NONE',  ( 1.000000000000000000, 0.000000000000000000, -0.000000000000000000 ) ) ;
#6233=ORIENTED_EDGE ( 'NONE', *, *, #4920, .F. ) ;
#6236=DIRECTION ( 'NONE',  ( 0.000000000000000000, 0.000000000000000000, -1.000000000000000000 ) ) ;
#6237=LINE ( 'NONE', #631, #5487 ) ;
#6238=DIRECTION ( 'NONE',  ( -1.000000000000000000, 4.270088556250607616E-16, 0.000000000000000000 ) ) ;
#6243=EDGE_LOOP ( 'NONE', ( #5714, #518, #3926, #711 ) ) ;
#6249=EDGE_CURVE ( 'NONE', #3234, #2065, #637, .T. ) ;
#6250=CARTESIAN_POINT ( 'NONE',  ( -37.50000000000000000, 4.857225732735047243E-14, 0.000000000000000000 ) ) ;
#6251=CARTESIAN_POINT ( 'NONE',  ( 339.1025403784437913, 75.00000000000005684, 125.0000000000000000 ) ) ;
#6252=CIRCLE ( 'NONE', #495, 12.49999999999999467 ) ;
#6258=EDGE_CURVE ( 'NONE', #4433, #4036, #4647, .T. ) ;
#6259=VERTEX_POINT ( 'NONE', #4055 ) ;
#6260=LINE ( 'NONE', #5659, #3940 ) ;
#6262=DIRECTION ( 'NONE',  ( 0.000000000000000000, 1.000000000000000000, -0.000000000000000000 ) ) ;
#6263=DIRECTION ( 'NONE',  ( 1.000000000000000000, 2.960594732333750117E-15, -0.000000000000000000 ) ) ;
#6269=CYLINDRICAL_SURFACE ( 'NONE', #1113, 12.50000000000001066 ) ;
#6270=FACE_OUTER_BOUND ( 'NONE', #6986, .T. ) ;
#6272=DIRECTION ( 'NONE',  ( -0.000000000000000000, -0.000000000000000000, -1.000000000000000000 ) ) ;
#6278=DIRECTION ( 'NONE',  ( -0.000000000000000000, 0.000000000000000000, 1.000000000000000000 ) ) ;
#6280=EDGE_CURVE ( 'NONE', #6088, #7780, #7171, .T. ) ;
#6282=ORIENTED_EDGE ( 'NONE', *, *, #3653, .T. ) ;
#6286=CARTESIAN_POINT ( 'NONE',  ( 162.5000000000000000, 37.50000000000006395, 0.000000000000000000 ) ) ;
#6294=DIRECTION ( 'NONE',  ( -4.789677997474686366E-16, -1.000000000000000000, -0.000000000000000000 ) ) ;
#6297=DIRECTION ( 'NONE',  ( -0.000000000000000000, -0.000000000000000000, -1.000000000000000000 ) ) ;
#6300=EDGE_LOOP ( 'NONE', ( #640, #1375, #4593, #4033 ) ) ;
#6306=DIRECTION ( 'NONE',  ( -1.000000000000000000, 0.000000000000000000, 0.000000000000000000 ) ) ;
#6310=ORIENTED_EDGE ( 'NONE', *, *, #6839, .F. ) ;
#6316=DIRECTION ( 'NONE',  ( 1.000000000000000000, 0.000000000000000000, 0.000000000000000000 ) ) ;
#6317=DIRECTION ( 'NONE',  ( 1.000000000000000000, -1.295260195396012940E-15, 0.000000000000000000 ) ) ;
#6319=ORIENTED_EDGE ( 'NONE', *, *, #2649, .T. ) ;
#6320=EDGE_CURVE ( 'NONE', #1477, #1859, #4986, .T. ) ;
#6322=ORIENTED_EDGE ( 'NONE', *, *, #6249, .F. ) ;
#6323=LINE ( 'NONE', #229, #4548 ) ;
#6324=VECTOR ( 'NONE', #3025, 1000.000000000000000 ) ;
#6325=FACE_OUTER_BOUND ( 'NONE', #2000, .T. ) ;
#6326=DIRECTION ( 'NONE',  ( 0.000000000000000000, 0.000000000000000000, 1.000000000000000000 ) ) ;
#6327=DIRECTION ( 'NONE',  ( -0.000000000000000000, 0.000000000000000000, 1.000000000000000000 ) ) ;
#6329=AXIS2_PLACEMENT_3D ( 'NONE', #7392, #3142, #5049 ) ;
#6330=ORIENTED_EDGE ( 'NONE', *, *, #1018, .T. ) ;
#6331=AXIS2_PLACEMENT_3D ( 'NONE', #2099, #5837, #4619 ) ;
#6332=CARTESIAN_POINT ( 'NONE',  ( 200.0000000000000000, 0.000000000000000000, 12.50000000000000000 ) ) ;
#6333=ORIENTED_EDGE ( 'NONE', *, *, #6280, .T. ) ;
#6334=ORIENTED_EDGE ( 'NONE', *, *, #4046, .T. ) ;
#6338=ORIENTED_EDGE ( 'NONE', *, *, #1693, .F. ) ;
#6342=DIRECTION ( 'NONE',  ( 0.000000000000000000, 0.000000000000000000, 1.000000000000000000 ) ) ;
#6347=AXIS2_PLACEMENT_3D ( 'NONE', #3453, #5976, #1557 ) ;
#6352=ORIENTED_EDGE ( 'NONE', *, *, #6411, .T. ) ;
#6354=CARTESIAN_POINT ( 'NONE',  ( 5.204170427930428856E-14, 37.50000000000005684, 12.50000000000000000 ) ) ;
#6355=EDGE_CURVE ( 'NONE', #2065, #30, #6742, .T. ) ;
#6356=CARTESIAN_POINT ( 'NONE',  ( 412.5000000000000568, 75.00000000000001421, 5.000000000000000000 ) ) ;
#6357=ORIENTED_EDGE ( 'NONE', *, *, #2342, .T. ) ;
#6360=VERTEX_POINT ( 'NONE', #1324 ) ;
#6365=CIRCLE ( 'NONE', #3166, 12.50000000000001066 ) ;
#6366=PLANE ( 'NONE',  #1446 ) ;
#6367=PLANE ( 'NONE',  #6637 ) ;
#6369=CIRCLE ( 'NONE', #5346, 5.000000000000000888 ) ;
#6374=CARTESIAN_POINT ( 'NONE',  ( 212.5000000000000284, 1.530808498934191127E-15, 0.000000000000000000 ) ) ;
#6381=VECTOR ( 'NONE', #4421, 1000.000000000000000 ) ;
#6382=ORIENTED_EDGE ( 'NONE', *, *, #6021, .F. ) ;
#6387=CIRCLE ( 'NONE', #6526, 29.99999999999997158 ) ;
#6390=CARTESIAN_POINT ( 'NONE',  ( -27.49999999999994671, 47.50000000000009237, 0.000000000000000000 ) ) ;
#6396=CARTESIAN_POINT ( 'NONE',  ( -37.49999999999989342, 177.4999999999999432, 130.0000000000000000 ) ) ;
#6404=EDGE_CURVE ( 'NONE', #7046, #3816, #1144, .T. ) ;
#6406=ORIENTED_EDGE ( 'NONE', *, *, #946, .T. ) ;
#6407=LINE ( 'NONE', #3442, #602 ) ;
#6410=LINE ( 'NONE', #3360, #5172 ) ;
#6411=EDGE_CURVE ( 'NONE', #1547, #1382, #3180, .T. ) ;
#6413=CARTESIAN_POINT ( 'NONE',  ( 52.50000000000000711, 111.9999999999998863, 130.0000000000000000 ) ) ;
#6419=CARTESIAN_POINT ( 'NONE',  ( 42.50000000000000711, 177.5000000000000000, 12.65877081724072362 ) ) ;
#6420=( GEOMETRIC_REPRESENTATION_CONTEXT ( 3 ) GLOBAL_UNCERTAINTY_ASSIGNED_CONTEXT ( ( #5525 ) ) GLOBAL_UNIT_ASSIGNED_CONTEXT ( ( #5434, #5964, #2839 ) ) REPRESENTATION_CONTEXT ( 'NONE', 'WORKASPACE' ) );
#6422=EDGE_CURVE ( 'NONE', #846, #2024, #6823, .T. ) ;
#6430=CARTESIAN_POINT ( 'NONE',  ( 296.6025403784439618, 217.5000000000000568, 125.0000000000000000 ) ) ;
#6432=CARTESIAN_POINT ( 'NONE',  ( 296.6025403784437913, 82.50000000000004263, 17.49999999999998934 ) ) ;
#6435=ORIENTED_EDGE ( 'NONE', *, *, #5650, .T. ) ;
#6436=ORIENTED_EDGE ( 'NONE', *, *, #4134, .T. ) ;
#6438=CARTESIAN_POINT ( 'NONE',  ( 291.6025403784437913, 135.0000000000000000, 0.000000000000000000 ) ) ;
#6440=CARTESIAN_POINT ( 'NONE',  ( 296.6025403784439050, 90.00000000000001421, 12.50000000000000000 ) ) ;
#6444=CIRCLE ( 'NONE', #2997, 5.000000000000004441 ) ;
#6447=ORIENTED_EDGE ( 'NONE', *, *, #2255, .T. ) ;
#6448=VECTOR ( 'NONE', #4901, 1000.000000000000000 ) ;
#6453=ORIENTED_EDGE ( 'NONE', *, *, #4950, .F. ) ;
#6457=LINE ( 'NONE', #3495, #5948 ) ;
#6458=AXIS2_PLACEMENT_3D ( 'NONE', #6148, #4447, #5628 ) ;
#6459=VECTOR ( 'NONE', #2022, 1000.000000000000000 ) ;
#6460=ORIENTED_EDGE ( 'NONE', *, *, #2070, .F. ) ;
#6465=DIRECTION ( 'NONE',  ( 0.000000000000000000, 0.000000000000000000, 1.000000000000000000 ) ) ;
#6469=VECTOR ( 'NONE', #948, 1000.000000000000000 ) ;
#6470=CIRCLE ( 'NONE', #2627, 29.99999999999997158 ) ;
#6473=ORIENTED_EDGE ( 'NONE', *, *, #2919, .T. ) ;
#6475=DIRECTION ( 'NONE',  ( -0.000000000000000000, -0.000000000000000000, -1.000000000000000000 ) ) ;
#6476=VECTOR ( 'NONE', #4313, 1000.000000000000000 ) ;
#6477=CARTESIAN_POINT ( 'NONE',  ( 412.5000000000000568, 75.00000000000001421, 5.000000000000000000 ) ) ;
#6479=ORIENTED_EDGE ( 'NONE', *, *, #5774, .F. ) ;
#6481=EDGE_LOOP ( 'NONE', ( #4579, #5776 ) ) ;
#6485=VERTEX_POINT ( 'NONE', #3853 ) ;
#6493=AXIS2_PLACEMENT_3D ( 'NONE', #4411, #2010, #1929 ) ;
#6494=CARTESIAN_POINT ( 'NONE',  ( 412.4999999999998863, 82.50000000000004263, 17.49999999999998934 ) ) ;
#6496=DIRECTION ( 'NONE',  ( 1.000000000000000000, -9.251858538542979716E-16, 0.000000000000000000 ) ) ;
#6497=ORIENTED_EDGE ( 'NONE', *, *, #76, .T. ) ;
#6499=DIRECTION ( 'NONE',  ( -1.000000000000000000, 0.000000000000000000, -0.000000000000000000 ) ) ;
#6502=EDGE_CURVE ( 'NONE', #3550, #2505, #4444, .T. ) ;
#6506=ORIENTED_EDGE ( 'NONE', *, *, #2979, .F. ) ;
#6515=VECTOR ( 'NONE', #5106, 1000.000000000000000 ) ;
#6519=VERTEX_POINT ( 'NONE', #283 ) ;
#6521=DIRECTION ( 'NONE',  ( -0.000000000000000000, -0.000000000000000000, -1.000000000000000000 ) ) ;
#6523=DIRECTION ( 'NONE',  ( -1.000000000000000000, 0.000000000000000000, 0.000000000000000000 ) ) ;
#6525=ORIENTED_EDGE ( 'NONE', *, *, #1400, .T. ) ;
#6526=AXIS2_PLACEMENT_3D ( 'NONE', #4859, #7316, #4257 ) ;
#6529=ORIENTED_EDGE ( 'NONE', *, *, #7065, .F. ) ;
#6530=ORIENTED_EDGE ( 'NONE', *, *, #3168, .T. ) ;
#6533=DIRECTION ( 'NONE',  ( -0.000000000000000000, -0.000000000000000000, -1.000000000000000000 ) ) ;
#6535=DIRECTION ( 'NONE',  ( 0.000000000000000000, -1.000000000000000000, 0.000000000000000000 ) ) ;
#6537=ORIENTED_EDGE ( 'NONE', *, *, #1940, .F. ) ;
#6541=ORIENTED_EDGE ( 'NONE', *, *, #5473, .F. ) ;
#6545=VERTEX_POINT ( 'NONE', #2729 ) ;
#6548=DIRECTION ( 'NONE',  ( 1.000000000000000000, 4.789677997474691297E-16, -0.000000000000000000 ) ) ;
#6549=AXIS2_PLACEMENT_3D ( 'NONE', #6438, #2796, #4626 ) ;
#6552=ADVANCED_FACE ( 'NONE', ( #6978 ), #1957, .T. ) ;
#6557=EDGE_LOOP ( 'NONE', ( #4542, #4248, #7713, #2787, #4166 ) ) ;
#6568=PLANE ( 'NONE',  #3314 ) ;
#6576=DIRECTION ( 'NONE',  ( 1.000000000000000000, 0.000000000000000000, 0.000000000000000000 ) ) ;
#6578=VERTEX_POINT ( 'NONE', #842 ) ;
#6583=CARTESIAN_POINT ( 'NONE',  ( 47.50000000000000711, 177.5000000000000000, 5.000000000000000000 ) ) ;
#6584=VECTOR ( 'NONE', #6067, 1000.000000000000000 ) ;
#6585=VECTOR ( 'NONE', #3682, 999.9999999999998863 ) ;
#6586=LINE ( 'NONE', #7793, #6584 ) ;
#6588=VECTOR ( 'NONE', #6189, 1000.000000000000000 ) ;
#6589=CIRCLE ( 'NONE', #5440, 37.50000000000000711 ) ;
#6590=FACE_OUTER_BOUND ( 'NONE', #2845, .T. ) ;
#6592=VERTEX_POINT ( 'NONE', #883 ) ;
#6593=EDGE_CURVE ( 'NONE', #2348, #4343, #234, .T. ) ;
#6595=CARTESIAN_POINT ( 'NONE',  ( 286.6025403784439050, 0.000000000000000000, 12.50000000000000000 ) ) ;
#6597=ORIENTED_EDGE ( 'NONE', *, *, #2533, .F. ) ;
#6601=CIRCLE ( 'NONE', #2449, 12.49999999999999467 ) ;
#6607=CARTESIAN_POINT ( 'NONE',  ( 46.25000000000002842, 111.9999999999999005, 130.0000000000000000 ) ) ;
#6610=CARTESIAN_POINT ( 'NONE',  ( 162.5000000000000000, 112.5000000000000142, 0.000000000000000000 ) ) ;
#6612=ORIENTED_EDGE ( 'NONE', *, *, #3611, .F. ) ;
#6613=ADVANCED_FACE ( 'NONE', ( #7099 ), #5332, .F. ) ;
#6617=VERTEX_POINT ( 'NONE', #7819 ) ;
#6618=CARTESIAN_POINT ( 'NONE',  ( 37.50000000000000711, 42.50000000000003553, 12.50000000000000000 ) ) ;
#6619=DIRECTION ( 'NONE',  ( 0.000000000000000000, -1.000000000000000000, 0.000000000000000000 ) ) ;
#6620=CIRCLE ( 'NONE', #1875, 5.000000000000000000 ) ;
#6622=ORIENTED_EDGE ( 'NONE', *, *, #2721, .F. ) ;
#6628=CARTESIAN_POINT ( 'NONE',  ( 212.5000000000000284, 1.530808498934191127E-15, 12.50000000000000000 ) ) ;
#6631=DIRECTION ( 'NONE',  ( 0.000000000000000000, 1.000000000000000000, -0.000000000000000000 ) ) ;
#6635=CARTESIAN_POINT ( 'NONE',  ( -27.49999999999994671, 47.50000000000009237, 12.65877081724073783 ) ) ;
#6637=AXIS2_PLACEMENT_3D ( 'NONE', #232, #3805, #2681 ) ;
#6642=VERTEX_POINT ( 'NONE', #5203 ) ;
#6644=DIRECTION ( 'NONE',  ( 0.000000000000000000, 0.000000000000000000, 1.000000000000000000 ) ) ;
#6645=LINE ( 'NONE', #7130, #686 ) ;
#6646=ORIENTED_EDGE ( 'NONE', *, *, #4852, .T. ) ;
#6651=EDGE_CURVE ( 'NONE', #5267, #4433, #3184, .T. ) ;
#6652=ORIENTED_EDGE ( 'NONE', *, *, #1420, .F. ) ;
#6654=CYLINDRICAL_SURFACE ( 'NONE', #4983, 12.50000000000001066 ) ;
#6656=CIRCLE ( 'NONE', #1909, 12.50000000000001066 ) ;
#6658=VECTOR ( 'NONE', #3648, 1000.000000000000000 ) ;
#6660=LINE ( 'NONE', #7892, #2253 ) ;
#6661=EDGE_CURVE ( 'NONE', #2900, #5478, #4836, .T. ) ;
#6666=DIRECTION ( 'NONE',  ( 1.000000000000000000, 0.000000000000000000, 0.000000000000000000 ) ) ;
#6667=CARTESIAN_POINT ( 'NONE',  ( 353.4483633286965301, 217.5000000000000284, 138.3903618369216417 ) ) ;
#6669=CARTESIAN_POINT ( 'NONE',  ( 46.25000000000002842, 47.50000000000003553, 130.0000000000000000 ) ) ;
#6672=PRODUCT_CONTEXT ( 'NONE', #2184, 'mechanical' ) ;
#6674=CARTESIAN_POINT ( 'NONE',  ( -27.08354679051378255, 47.50000000000009948, 12.55124306091977182 ) ) ;
#6675=PLANE ( 'NONE',  #3003 ) ;
#6677=ORIENTED_EDGE ( 'NONE', *, *, #2987, .F. ) ;
#6679=DIRECTION ( 'NONE',  ( 0.000000000000000000, 0.000000000000000000, 1.000000000000000000 ) ) ;
#6681=CARTESIAN_POINT ( 'NONE',  ( -27.49999999999989342, 182.4999999999999432, 12.50000000000000000 ) ) ;
#6685=DIRECTION ( 'NONE',  ( 1.000000000000000000, 0.000000000000000000, 0.000000000000000000 ) ) ;
#6691=EDGE_LOOP ( 'NONE', ( #1791, #7048, #4318, #6770 ) ) ;
#6692=EDGE_CURVE ( 'NONE', #3005, #7842, #7656, .T. ) ;
#6693=DIRECTION ( 'NONE',  ( 0.000000000000000000, -0.000000000000000000, -1.000000000000000000 ) ) ;
#6695=EDGE_CURVE ( 'NONE', #5006, #6642, #4606, .T. ) ;
#6699=PLANE ( 'NONE',  #4831 ) ;
#6702=CARTESIAN_POINT ( 'NONE',  ( 162.5000000000000000, 112.5000000000000142, 12.50000000000000000 ) ) ;
#6703=CARTESIAN_POINT ( 'NONE',  ( -4.731064025391297956E-15, 37.50000000000004263, 0.000000000000000000 ) ) ;
#6705=CARTESIAN_POINT ( 'NONE',  ( 52.50000000000000711, 111.9999999999999858, 130.0000000000000000 ) ) ;
#6706=VECTOR ( 'NONE', #3067, 1000.000000000000000 ) ;
#6712=DIRECTION ( 'NONE',  ( -0.000000000000000000, -0.000000000000000000, -1.000000000000000000 ) ) ;
#6715=ORIENTED_EDGE ( 'NONE', *, *, #2157, .T. ) ;
#6716=DIRECTION ( 'NONE',  ( 1.000000000000000000, 0.000000000000000000, 0.000000000000000000 ) ) ;
#6721=CIRCLE ( 'NONE', #3893, 12.50000000000000000 ) ;
#6722=EDGE_CURVE ( 'NONE', #5081, #2041, #3307, .T. ) ;
#6723=DIRECTION ( 'NONE',  ( -0.000000000000000000, -0.000000000000000000, -1.000000000000000000 ) ) ;
#6731=FACE_OUTER_BOUND ( 'NONE', #3762, .T. ) ;
#6734=ORIENTED_EDGE ( 'NONE', *, *, #5163, .F. ) ;
#6739=EDGE_CURVE ( 'NONE', #5478, #7566, #2974, .T. ) ;
#6742=LINE ( 'NONE', #4214, #1910 ) ;
#6743=CARTESIAN_POINT ( 'NONE',  ( 12.50000000000000000, 1.530808498934191521E-15, 0.000000000000000000 ) ) ;
#6744=LINE ( 'NONE', #4407, #2237 ) ;
#6747=EDGE_CURVE ( 'NONE', #2269, #6578, #1759, .T. ) ;
#6748=CARTESIAN_POINT ( 'NONE',  ( 291.6025403784439050, 90.00000000000001421, 12.50000000000000000 ) ) ;
#6750=EDGE_CURVE ( 'NONE', #7220, #7046, #4880, .T. ) ;
#6755=CARTESIAN_POINT ( 'NONE',  ( 199.9999999999998863, 225.0000000000000284, 12.50000000000000000 ) ) ;
#6760=ORIENTED_EDGE ( 'NONE', *, *, #7483, .T. ) ;
#6763=AXIS2_PLACEMENT_3D ( 'NONE', #4484, #7616, #7577 ) ;
#6770=ORIENTED_EDGE ( 'NONE', *, *, #2314, .T. ) ;
#6771=EDGE_CURVE ( 'NONE', #7160, #2126, #6252, .T. ) ;
#6773=VERTEX_POINT ( 'NONE', #6814 ) ;
#6775=ORIENTED_EDGE ( 'NONE', *, *, #4894, .F. ) ;
#6776=CARTESIAN_POINT ( 'NONE',  ( 232.4759526419164786, -18.74999999999998934, 12.50000000000000000 ) ) ;
#6780=CIRCLE ( 'NONE', #1656, 12.50000000000001066 ) ;
#6783=EDGE_LOOP ( 'NONE', ( #5363, #6001, #2202, #6233 ) ) ;
#6784=DIRECTION ( 'NONE',  ( -1.000000000000000000, 0.000000000000000000, 0.000000000000000000 ) ) ;
#6785=DIRECTION ( 'NONE',  ( -0.000000000000000000, -0.000000000000000000, -1.000000000000000000 ) ) ;
#6787=LINE ( 'NONE', #7390, #7089 ) ;
#6788=CARTESIAN_POINT ( 'NONE',  ( -37.49999999999989342, 177.4999999999999432, 12.50000000000000000 ) ) ;
#6790=CARTESIAN_POINT ( 'NONE',  ( 162.4999999999999432, 187.4999999999999716, 12.50000000000000000 ) ) ;
#6794=ADVANCED_FACE ( 'NONE', ( #7852, #6731, #3609, #1195, #3695, #675 ), #1916, .F. ) ;
#6798=APPLICATION_CONTEXT ( 'automotive_design' ) ;
#6805=VERTEX_POINT ( 'NONE', #4203 ) ;
#6812=CARTESIAN_POINT ( 'NONE',  ( 49.37500000000001421, 112.5000000000000142, 195.4980915752512658 ) ) ;
#6814=CARTESIAN_POINT ( 'NONE',  ( -27.49999999999994671, 37.50000000000008527, 12.50000000000000000 ) ) ;
#6819=EDGE_LOOP ( 'NONE', ( #7697, #6597, #3800, #2768 ) ) ;
#6821=AXIS2_PLACEMENT_3D ( 'NONE', #4692, #7153, #2494 ) ;
#6823=LINE ( 'NONE', #2569, #2170 ) ;
#6832=VECTOR ( 'NONE', #5248, 1000.000000000000000 ) ;
#6833=ADVANCED_FACE ( 'NONE', ( #2481 ), #1392, .F. ) ;
#6839=EDGE_CURVE ( 'NONE', #600, #2766, #4393, .T. ) ;
#6842=CIRCLE ( 'NONE', #4269, 5.000000000000004441 ) ;
#6845=ADVANCED_FACE ( 'NONE', ( #5004, #3281 ), #6367, .F. ) ;
#6850=AXIS2_PLACEMENT_3D ( 'NONE', #3119, #634, #403 ) ;
#6851=ORIENTED_EDGE ( 'NONE', *, *, #3656, .T. ) ;
#6854=FACE_OUTER_BOUND ( 'NONE', #843, .T. ) ;
#6855=DIRECTION ( 'NONE',  ( -1.000000000000000000, 4.270088556250607616E-16, -0.000000000000000000 ) ) ;
#6856=AXIS2_PLACEMENT_3D ( 'NONE', #489, #4846, #1164 ) ;
#6862=ORIENTED_EDGE ( 'NONE', *, *, #76, .F. ) ;
#6866=ORIENTED_EDGE ( 'NONE', *, *, #2349, .F. ) ;
#6868=AXIS2_PLACEMENT_3D ( 'NONE', #5145, #5805, #1582 ) ;
#6874=CARTESIAN_POINT ( 'NONE',  ( 42.50000000000000711, 177.5000000000000000, 12.50000000000000000 ) ) ;
#6875=CARTESIAN_POINT ( 'NONE',  ( 46.25000000000002842, 47.50000000000003553, 17.50000000000001421 ) ) ;
#6879=EDGE_LOOP ( 'NONE', ( #2075, #7611, #7055, #2604 ) ) ;
#6881=DIRECTION ( 'NONE',  ( 0.000000000000000000, 1.000000000000000000, 0.000000000000000000 ) ) ;
#6887=AXIS2_PLACEMENT_3D ( 'NONE', #5581, #7345, #3657 ) ;
#6890=LINE ( 'NONE', #5002, #1737 ) ;
#6895=ADVANCED_FACE ( 'NONE', ( #6854 ), #7607, .F. ) ;
#6897=ADVANCED_FACE ( 'NONE', ( #2640 ), #7011, .T. ) ;
#6906=DIRECTION ( 'NONE',  ( 0.000000000000000000, 1.000000000000000000, 0.000000000000000000 ) ) ;
#6907=ORIENTED_EDGE ( 'NONE', *, *, #1027, .T. ) ;
#6911=VECTOR ( 'NONE', #6105, 1000.000000000000000 ) ;
#6914=CARTESIAN_POINT ( 'NONE',  ( 286.6025403784439050, 75.00000000000002842, 0.000000000000000000 ) ) ;
#6923=DIRECTION ( 'NONE',  ( -0.000000000000000000, -0.000000000000000000, -1.000000000000000000 ) ) ;
#6925=ORIENTED_EDGE ( 'NONE', *, *, #2206, .T. ) ;
#6927=DIRECTION ( 'NONE',  ( 0.000000000000000000, 0.000000000000000000, 1.000000000000000000 ) ) ;
#6929=DIRECTION ( 'NONE',  ( 0.000000000000000000, 0.000000000000000000, 1.000000000000000000 ) ) ;
#6930=EDGE_LOOP ( 'NONE', ( #74, #3080 ) ) ;
#6931=PLANE ( 'NONE',  #627 ) ;
#6940=DIRECTION ( 'NONE',  ( -1.000000000000000000, -1.295260195396013137E-15, 0.000000000000000000 ) ) ;
#6941=CARTESIAN_POINT ( 'NONE',  ( 326.6025403784437913, 142.5000000000000000, 125.0000000000000000 ) ) ;
#6942=CARTESIAN_POINT ( 'NONE',  ( 412.5000000000002274, 1.221245327087672598E-12, 12.50000000000000000 ) ) ;
#6946=ADVANCED_FACE ( 'NONE', ( #2033, #4476 ), #6931, .F. ) ;
#6949=CYLINDRICAL_SURFACE ( 'NONE', #4533, 65.50000000000000000 ) ;
#6952=ORIENTED_EDGE ( 'NONE', *, *, #3855, .F. ) ;
#6965=LINE ( 'NONE', #6812, #7626 ) ;
#6966=VECTOR ( 'NONE', #3377, 1000.000000000000000 ) ;
#6971=VECTOR ( 'NONE', #7409, 1000.000000000000000 ) ;
#6975=ORIENTED_EDGE ( 'NONE', *, *, #1111, .F. ) ;
#6978=FACE_OUTER_BOUND ( 'NONE', #6219, .T. ) ;
#6985=ADVANCED_FACE ( 'NONE', ( #5279 ), #2284, .F. ) ;
#6986=EDGE_LOOP ( 'NONE', ( #7557, #450, #7636, #3384 ) ) ;
#6991=VECTOR ( 'NONE', #186, 1000.000000000000000 ) ;
#6992=ADVANCED_FACE ( 'NONE', ( #5891 ), #6568, .F. ) ;
#6994=ADVANCED_FACE ( 'NONE', ( #350 ), #3993, .F. ) ;
#6999=FACE_OUTER_BOUND ( 'NONE', #193, .T. ) ;
#7000=FACE_OUTER_BOUND ( 'NONE', #4702, .T. ) ;
#7005=LINE ( 'NONE', #3874, #3837 ) ;
#7008=VECTOR ( 'NONE', #2656, 1000.000000000000000 ) ;
#7009=CARTESIAN_POINT ( 'NONE',  ( -26.66645320948611442, 177.5512430609197168, 12.50000000000001421 ) ) ;
#7011=PLANE ( 'NONE',  #3447 ) ;
#7012=PLANE ( 'NONE',  #4155 ) ;
#7017=ORIENTED_EDGE ( 'NONE', *, *, #2070, .T. ) ;
#7020=VECTOR ( 'NONE', #5453, 1000.000000000000000 ) ;
#7021=CARTESIAN_POINT ( 'NONE',  ( 286.6025403784437913, 150.0000000000000284, 0.000000000000000000 ) ) ;
#7028=CARTESIAN_POINT ( 'NONE',  ( -31.24999999999997158, 113.0000000000000995, 130.0000000000000000 ) ) ;
#7029=DIRECTION ( 'NONE',  ( -0.000000000000000000, -0.000000000000000000, -1.000000000000000000 ) ) ;
#7032=CIRCLE ( 'NONE', #2809, 32.75000000000000000 ) ;
#7033=CIRCLE ( 'NONE', #2804, 12.50000000000001066 ) ;
#7034=CYLINDRICAL_SURFACE ( 'NONE', #5963, 12.50000000000001066 ) ;
#7039=ADVANCED_FACE ( 'NONE', ( #7590, #7476 ), #1034, .F. ) ;
#7040=DIRECTION ( 'NONE',  ( 0.000000000000000000, -0.000000000000000000, -1.000000000000000000 ) ) ;
#7043=FACE_BOUND ( 'NONE', #3278, .T. ) ;
#7046=VERTEX_POINT ( 'NONE', #6390 ) ;
#7048=ORIENTED_EDGE ( 'NONE', *, *, #4428, .F. ) ;
#7051=DIRECTION ( 'NONE',  ( -1.000000000000000000, 0.000000000000000000, 0.000000000000000000 ) ) ;
#7055=ORIENTED_EDGE ( 'NONE', *, *, #6258, .T. ) ;
#7057=ORIENTED_EDGE ( 'NONE', *, *, #1177, .F. ) ;
#7058=CARTESIAN_POINT ( 'NONE',  ( 42.50000000000000711, 187.5000000000000000, 12.50000000000000000 ) ) ;
#7059=EDGE_CURVE ( 'NONE', #7780, #530, #2055, .T. ) ;
#7065=EDGE_CURVE ( 'NONE', #4126, #6519, #183, .T. ) ;
#7068=CYLINDRICAL_SURFACE ( 'NONE', #242, 4.999999999999997335 ) ;
#7069=CARTESIAN_POINT ( 'NONE',  ( -27.49999999999989342, 177.4999999999999432, 0.000000000000000000 ) ) ;
#7070=CARTESIAN_POINT ( 'NONE',  ( 62.50000000000009948, 144.7499999999999147, 130.0000000000000000 ) ) ;
#7074=ORIENTED_EDGE ( 'NONE', *, *, #3090, .F. ) ;
#7076=LINE ( 'NONE', #294, #7744 ) ;
#7085=CYLINDRICAL_SURFACE ( 'NONE', #6868, 5.000000000000000888 ) ;
#7088=CARTESIAN_POINT ( 'NONE',  ( 37.50000000000000711, 42.50000000000003553, 12.50000000000000000 ) ) ;
#7089=VECTOR ( 'NONE', #7271, 1000.000000000000000 ) ;
#7093=CIRCLE ( 'NONE', #318, 37.50000000000000000 ) ;
#7094=CARTESIAN_POINT ( 'NONE',  ( 296.6025403784437913, 144.9999999999999716, 5.000000000000000000 ) ) ;
#7096=CARTESIAN_POINT ( 'NONE',  ( -26.24999999999997158, 177.6587708172406224, 12.50000000000000000 ) ) ;
#7099=FACE_OUTER_BOUND ( 'NONE', #5880, .T. ) ;
#7105=ORIENTED_EDGE ( 'NONE', *, *, #237, .F. ) ;
#7108=CIRCLE ( 'NONE', #51, 32.75000000000000000 ) ;
#7111=DIRECTION ( 'NONE',  ( 0.000000000000000000, -0.000000000000000000, -1.000000000000000000 ) ) ;
#7112=CARTESIAN_POINT ( 'NONE',  ( 187.5000000000000000, 0.000000000000000000, 0.000000000000000000 ) ) ;
#7113=CARTESIAN_POINT ( 'NONE',  ( 52.50000000000000711, 79.24999999999987210, 130.0000000000000000 ) ) ;
#7116=CARTESIAN_POINT ( 'NONE',  ( 296.6025403784439050, 0.000000000000000000, 12.50000000000000000 ) ) ;
#7117=ORIENTED_EDGE ( 'NONE', *, *, #5420, .F. ) ;
#7118=CARTESIAN_POINT ( 'NONE',  ( 232.4759526419164217, 243.7500000000000000, 12.50000000000000000 ) ) ;
#7120=AXIS2_PLACEMENT_3D ( 'NONE', #4194, #7293, #1792 ) ;
#7126=ORIENTED_EDGE ( 'NONE', *, *, #2877, .T. ) ;
#7130=CARTESIAN_POINT ( 'NONE',  ( 412.5000000000001137, 217.5000000000000000, 20.00000000000000000 ) ) ;
#7131=EDGE_LOOP ( 'NONE', ( #4404, #7652, #7182, #5897, #7259, #4865, #6479, #7703, #6322, #7265, #6338, #1318, #3089, #2561, #2092, #1697, #6091, #4416, #1077, #2978, #4424, #2758, #5913, #764 ) ) ;
#7136=AXIS2_PLACEMENT_3D ( 'NONE', #2181, #1023, #3347 ) ;
#7137=DIRECTION ( 'NONE',  ( -0.000000000000000000, -0.000000000000000000, -1.000000000000000000 ) ) ;
#7141=ADVANCED_FACE ( 'NONE', ( #2621 ), #5058, .F. ) ;
#7143=LINE ( 'NONE', #4088, #4282 ) ;
#7147=EDGE_LOOP ( 'NONE', ( #3830, #7402, #2894, #5821 ) ) ;
#7152=DIRECTION ( 'NONE',  ( 0.000000000000000000, 0.000000000000000000, -1.000000000000000000 ) ) ;
#7153=DIRECTION ( 'NONE',  ( 1.000000000000000000, 0.000000000000000000, 0.000000000000000000 ) ) ;
#7154=CARTESIAN_POINT ( 'NONE',  ( 42.50000000000000000, 42.50000000000003553, 12.50000000000000000 ) ) ;
#7155=DIRECTION ( 'NONE',  ( -1.000000000000000000, 0.000000000000000000, 0.000000000000000000 ) ) ;
#7160=VERTEX_POINT ( 'NONE', #4136 ) ;
#7167=DIRECTION ( 'NONE',  ( 1.000000000000000000, 0.000000000000000000, 0.000000000000000000 ) ) ;
#7171=CIRCLE ( 'NONE', #372, 30.00000000000000000 ) ;
#7175=CYLINDRICAL_SURFACE ( 'NONE', #3285, 5.000000000000000000 ) ;
#7176=FACE_OUTER_BOUND ( 'NONE', #7262, .T. ) ;
#7181=DIRECTION ( 'NONE',  ( 0.000000000000000000, 1.000000000000000000, -0.000000000000000000 ) ) ;
#7182=ORIENTED_EDGE ( 'NONE', *, *, #5514, .F. ) ;
#7183=ADVANCED_FACE ( 'NONE', ( #331 ), #2308, .F. ) ;
#7184=DIRECTION ( 'NONE',  ( 1.000000000000000000, 0.000000000000000000, 0.000000000000000000 ) ) ;
#7188=VERTEX_POINT ( 'NONE', #1660 ) ;
#7189=ADVANCED_FACE ( 'NONE', ( #505, #7199 ), #7796, .F. ) ;
#7191=EDGE_CURVE ( 'NONE', #7188, #4785, #5912, .T. ) ;
#7197=ADVANCED_FACE ( 'NONE', ( #6590 ), #7235, .F. ) ;
#7199=FACE_OUTER_BOUND ( 'NONE', #4718, .T. ) ;
#7201=ORIENTED_EDGE ( 'NONE', *, *, #579, .T. ) ;
#7203=FACE_OUTER_BOUND ( 'NONE', #4970, .T. ) ;
#7204=FACE_OUTER_BOUND ( 'NONE', #2963, .T. ) ;
#7217=DIRECTION ( 'NONE',  ( -1.000000000000000000, 0.000000000000000000, 0.000000000000000000 ) ) ;
#7220=VERTEX_POINT ( 'NONE', #1094 ) ;
#7221=DIRECTION ( 'NONE',  ( 1.000000000000000000, 0.000000000000000000, 0.000000000000000000 ) ) ;
#7225=ORIENTED_EDGE ( 'NONE', *, *, #374, .F. ) ;
#7231=CARTESIAN_POINT ( 'NONE',  ( -37.49999999999995026, 47.50000000000009237, 130.0000000000000000 ) ) ;
#7235=CYLINDRICAL_SURFACE ( 'NONE', #7284, 12.50000000000000000 ) ;
#7239=DIRECTION ( 'NONE',  ( 0.000000000000000000, 0.000000000000000000, 1.000000000000000000 ) ) ;
#7241=CYLINDRICAL_SURFACE ( 'NONE', #3021, 37.50000000000003553 ) ;
#7243=EDGE_CURVE ( 'NONE', #2325, #6102, #6780, .T. ) ;
#7249=AXIS2_PLACEMENT_3D ( 'NONE', #5418, #3543, #7863 ) ;
#7257=VECTOR ( 'NONE', #301, 1000.000000000000000 ) ;
#7258=CARTESIAN_POINT ( 'NONE',  ( 199.9999999999998863, 225.0000000000000284, 0.000000000000000000 ) ) ;
#7259=ORIENTED_EDGE ( 'NONE', *, *, #1207, .F. ) ;
#7262=EDGE_LOOP ( 'NONE', ( #6529, #1710, #178, #4561 ) ) ;
#7265=ORIENTED_EDGE ( 'NONE', *, *, #2877, .F. ) ;
#7271=DIRECTION ( 'NONE',  ( 0.000000000000000000, 1.000000000000000000, -0.000000000000000000 ) ) ;
#7273=DIRECTION ( 'NONE',  ( -0.000000000000000000, -0.000000000000000000, -1.000000000000000000 ) ) ;
#7277=LINE ( 'NONE', #6072, #5851 ) ;
#7283=ORIENTED_EDGE ( 'NONE', *, *, #1501, .T. ) ;
#7284=AXIS2_PLACEMENT_3D ( 'NONE', #4695, #4061, #1570 ) ;
#7287=EDGE_LOOP ( 'NONE', ( #3867, #3884, #2557, #3631 ) ) ;
#7288=CARTESIAN_POINT ( 'NONE',  ( 0.000000000000000000, 137.4999999999999716, 12.50000000000000000 ) ) ;
#7293=DIRECTION ( 'NONE',  ( 0.000000000000000000, 1.000000000000000000, 0.000000000000000000 ) ) ;
#7298=LINE ( 'NONE', #5449, #377 ) ;
#7300=AXIS2_PLACEMENT_3D ( 'NONE', #5368, #558, #3643 ) ;
#7316=DIRECTION ( 'NONE',  ( 4.789677997474691297E-16, -1.000000000000000000, 0.000000000000000000 ) ) ;
#7318=FACE_OUTER_BOUND ( 'NONE', #6879, .T. ) ;
#7321=FACE_OUTER_BOUND ( 'NONE', #1045, .T. ) ;
#7322=ORIENTED_EDGE ( 'NONE', *, *, #4966, .F. ) ;
#7323=EDGE_CURVE ( 'NONE', #1302, #7538, #3847, .T. ) ;
#7324=ORIENTED_EDGE ( 'NONE', *, *, #1491, .F. ) ;
#7329=ORIENTED_EDGE ( 'NONE', *, *, #1693, .T. ) ;
#7334=ORIENTED_EDGE ( 'NONE', *, *, #5562, .F. ) ;
#7340=CARTESIAN_POINT ( 'NONE',  ( 162.5000000000000000, 37.50000000000006395, 12.50000000000000000 ) ) ;
#7345=DIRECTION ( 'NONE',  ( -0.000000000000000000, 0.000000000000000000, 1.000000000000000000 ) ) ;
#7349=CARTESIAN_POINT ( 'NONE',  ( 42.50000000000000711, 177.5000000000000000, 12.65877081724072362 ) ) ;
#7350=DIRECTION ( 'NONE',  ( 1.000000000000000000, 2.960594732333750117E-15, -0.000000000000000000 ) ) ;
#7351=CLOSED_SHELL ( 'NONE', ( #4573, #1671, #2233, #6833, #4251, #7729, #5919, #1951, #6110, #6985, #3046, #7039, #3898, #6845, #7183, #6552, #1659, #317, #6994, #5893, #1201, #6156, #2093, #4585, #1838, #2783, #5726, #5059, #6895, #79, #6992, #7189, #1813, #5056, #425, #455, #3271, #3079, #7503, #6613, #531, #1986, #6897, #5374, #1107, #6946, #7197, #3441, #7668, #1880, #2731, #6794, #7843, #61, #834, #1123, #7659, #5273, #2882, #5377, #1252, #3952, #3318, #3913, #3689, #3361, #5050, #169, #7433, #219, #429, #7141, #2439, #26 ) ) ;
#7353=AXIS2_PLACEMENT_3D ( 'NONE', #7154, #7709, #1490 ) ;
#7359=CARTESIAN_POINT ( 'NONE',  ( 187.4999999999998863, 225.0000000000000284, 12.50000000000000000 ) ) ;
#7360=EDGE_CURVE ( 'NONE', #3018, #1497, #885, .T. ) ;
#7365=CARTESIAN_POINT ( 'NONE',  ( -12.50000000000000000, 0.000000000000000000, 12.50000000000000000 ) ) ;
#7367=CARTESIAN_POINT ( 'NONE',  ( 338.3083524847280614, 75.00000000000005684, 168.7439889854708213 ) ) ;
#7369=LINE ( 'NONE', #1790, #44 ) ;
#7371=LINE ( 'NONE', #104, #6476 ) ;
#7376=ORIENTED_EDGE ( 'NONE', *, *, #4737, .F. ) ;
#7378=ORIENTED_EDGE ( 'NONE', *, *, #1420, .T. ) ;
#7380=VECTOR ( 'NONE', #5813, 1000.000000000000000 ) ;
#7381=DIRECTION ( 'NONE',  ( 1.000000000000000000, 0.000000000000000000, 0.000000000000000000 ) ) ;
#7382=VERTEX_POINT ( 'NONE', #2602 ) ;
#7390=CARTESIAN_POINT ( 'NONE',  ( 296.6025403784437913, 0.000000000000000000, 12.50000000000000000 ) ) ;
#7392=CARTESIAN_POINT ( 'NONE',  ( -6.945033096338293890E-14, 144.9999999999998295, 5.000000000000000000 ) ) ;
#7394=EDGE_CURVE ( 'NONE', #3133, #5735, #4460, .T. ) ;
#7399=CARTESIAN_POINT ( 'NONE',  ( 326.6025403784438481, 150.0000000000000568, 125.0000000000000000 ) ) ;
#7400=CARTESIAN_POINT ( 'NONE',  ( 0.000000000000000000, 0.000000000000000000, 12.50000000000000000 ) ) ;
#7402=ORIENTED_EDGE ( 'NONE', *, *, #4728, .F. ) ;
#7404=EDGE_CURVE ( 'NONE', #3018, #6617, #5696, .T. ) ;
#7406=LINE ( 'NONE', #778, #3438 ) ;
#7407=AXIS2_PLACEMENT_3D ( 'NONE', #7857, #4851, #1806 ) ;
#7409=DIRECTION ( 'NONE',  ( -0.000000000000000000, -0.000000000000000000, -1.000000000000000000 ) ) ;
#7410=EDGE_LOOP ( 'NONE', ( #6525, #2851, #6612, #3246, #5531 ) ) ;
#7411=DIRECTION ( 'NONE',  ( -4.789677997474686366E-16, -1.000000000000000000, -0.000000000000000000 ) ) ;
#7413=EDGE_LOOP ( 'NONE', ( #2444, #2878, #224, #3212 ) ) ;
#7416=LINE ( 'NONE', #3165, #466 ) ;
#7417=ORIENTED_EDGE ( 'NONE', *, *, #1649, .T. ) ;
#7419=DIRECTION ( 'NONE',  ( -0.000000000000000000, -0.000000000000000000, -1.000000000000000000 ) ) ;
#7423=AXIS2_PLACEMENT_3D ( 'NONE', #4199, #3527, #5974 ) ;
#7430=CARTESIAN_POINT ( 'NONE',  ( 42.50000000000000711, 182.5000000000000000, 0.000000000000000000 ) ) ;
#7433=ADVANCED_FACE ( 'NONE', ( #2989 ), #5421, .F. ) ;
#7436=CARTESIAN_POINT ( 'NONE',  ( 200.0000000000000000, 0.000000000000000000, 12.50000000000000000 ) ) ;
#7439=EDGE_CURVE ( 'NONE', #4603, #2565, #6387, .T. ) ;
#7440=EDGE_CURVE ( 'NONE', #6592, #3133, #7806, .T. ) ;
#7445=LINE ( 'NONE', #3794, #6381 ) ;
#7448=EDGE_LOOP ( 'NONE', ( #7461, #1198, #2396, #4388, #3964, #6862 ) ) ;
#7450=FACE_OUTER_BOUND ( 'NONE', #2138, .T. ) ;
#7454=DIRECTION ( 'NONE',  ( -0.000000000000000000, -0.000000000000000000, -1.000000000000000000 ) ) ;
#7455=ORIENTED_EDGE ( 'NONE', *, *, #1897, .T. ) ;
#7457=CARTESIAN_POINT ( 'NONE',  ( 62.50000000000008527, 111.9999999999998863, 130.0000000000000000 ) ) ;
#7459=ORIENTED_EDGE ( 'NONE', *, *, #1449, .F. ) ;
#7461=ORIENTED_EDGE ( 'NONE', *, *, #3168, .F. ) ;
#7462=CARTESIAN_POINT ( 'NONE',  ( 52.50000000000000711, 177.5000000000000000, 12.50000000000000000 ) ) ;
#7463=CARTESIAN_POINT ( 'NONE',  ( -0.000000000000000000, 177.5000000000000000, 0.000000000000000000 ) ) ;
#7465=ORIENTED_EDGE ( 'NONE', *, *, #3667, .T. ) ;
#7469=CARTESIAN_POINT ( 'NONE',  ( 187.4999999999998863, 225.0000000000000284, 12.50000000000000000 ) ) ;
#7476=FACE_OUTER_BOUND ( 'NONE', #2512, .T. ) ;
#7478=EDGE_CURVE ( 'NONE', #6642, #4785, #6009, .T. ) ;
#7479=CYLINDRICAL_SURFACE ( 'NONE', #1262, 32.75000000000001421 ) ;
#7480=FACE_OUTER_BOUND ( 'NONE', #1337, .T. ) ;
#7481=CARTESIAN_POINT ( 'NONE',  ( -37.49999999999997158, 1.601283208593976678E-14, 5.000000000000000000 ) ) ;
#7482=ORIENTED_EDGE ( 'NONE', *, *, #661, .T. ) ;
#7483=EDGE_CURVE ( 'NONE', #3721, #3479, #7032, .T. ) ;
#7493=CARTESIAN_POINT ( 'NONE',  ( 0.000000000000000000, 187.4999999999999432, 12.50000000000000000 ) ) ;
#7495=VECTOR ( 'NONE', #5005, 1000.000000000000000 ) ;
#7497=ORIENTED_EDGE ( 'NONE', *, *, #4852, .F. ) ;
#7499=ORIENTED_EDGE ( 'NONE', *, *, #4350, .F. ) ;
#7500=VECTOR ( 'NONE', #2472, 1000.000000000000000 ) ;
#7501=VERTEX_POINT ( 'NONE', #5282 ) ;
#7503=ADVANCED_FACE ( 'NONE', ( #4600 ), #354, .T. ) ;
#7515=VERTEX_POINT ( 'NONE', #6494 ) ;
#7517=LINE ( 'NONE', #262, #3061 ) ;
#7523=VERTEX_POINT ( 'NONE', #836 ) ;
#7526=DIRECTION ( 'NONE',  ( 0.000000000000000000, 0.000000000000000000, 1.000000000000000000 ) ) ;
#7528=CARTESIAN_POINT ( 'NONE',  ( 46.25000000000002842, 113.0000000000000426, 130.0000000000000000 ) ) ;
#7531=CARTESIAN_POINT ( 'NONE',  ( 47.50000000000000711, 177.5000000000000000, 0.000000000000000000 ) ) ;
#7538=VERTEX_POINT ( 'NONE', #3999 ) ;
#7539=VECTOR ( 'NONE', #3344, 1000.000000000000000 ) ;
#7547=VECTOR ( 'NONE', #1175, 1000.000000000000000 ) ;
#7548=VECTOR ( 'NONE', #6906, 1000.000000000000000 ) ;
#7554=ORIENTED_EDGE ( 'NONE', *, *, #6000, .T. ) ;
#7555=DIRECTION ( 'NONE',  ( 4.789677997474691297E-16, -1.000000000000000000, 0.000000000000000000 ) ) ;
#7557=ORIENTED_EDGE ( 'NONE', *, *, #2189, .T. ) ;
#7558=FACE_OUTER_BOUND ( 'NONE', #6243, .T. ) ;
#7559=CARTESIAN_POINT ( 'NONE',  ( 46.25000000000002842, 47.50000000000003553, 195.5000000000000000 ) ) ;
#7560=LINE ( 'NONE', #2060, #2742 ) ;
#7563=ADVANCED_BREP_SHAPE_REPRESENTATION ( '', ( #4361, #5785 ), #6420 ) ;
#7565=DIRECTION ( 'NONE',  ( -4.789677997474686366E-16, -1.000000000000000000, -0.000000000000000000 ) ) ;
#7566=VERTEX_POINT ( 'NONE', #3330 ) ;
#7568=DIRECTION ( 'NONE',  ( 0.000000000000000000, 0.000000000000000000, 1.000000000000000000 ) ) ;
#7570=FACE_OUTER_BOUND ( 'NONE', #6819, .T. ) ;
#7571=EDGE_CURVE ( 'NONE', #5563, #905, #278, .T. ) ;
#7572=ORIENTED_EDGE ( 'NONE', *, *, #1985, .F. ) ;
#7574=ORIENTED_EDGE ( 'NONE', *, *, #7571, .F. ) ;
#7577=DIRECTION ( 'NONE',  ( 1.000000000000000000, 0.000000000000000000, 0.000000000000000000 ) ) ;
#7582=EDGE_CURVE ( 'NONE', #2766, #2146, #3452, .T. ) ;
#7584=EDGE_CURVE ( 'NONE', #6578, #1942, #7298, .T. ) ;
#7587=FACE_OUTER_BOUND ( 'NONE', #1681, .T. ) ;
#7589=VERTEX_POINT ( 'NONE', #7886 ) ;
#7590=FACE_BOUND ( 'NONE', #1902, .T. ) ;
#7592=ORIENTED_EDGE ( 'NONE', *, *, #6593, .F. ) ;
#7593=CARTESIAN_POINT ( 'NONE',  ( 42.50000000000000000, 47.50000000000003553, 0.000000000000000000 ) ) ;
#7603=EDGE_LOOP ( 'NONE', ( #6677, #2595, #7126, #7378 ) ) ;
#7604=CARTESIAN_POINT ( 'NONE',  ( -26.24999999999997158, 47.50000000000009237, 17.50000000000001421 ) ) ;
#7605=CARTESIAN_POINT ( 'NONE',  ( -27.49999999999989342, 177.4999999999999432, 12.65877081724072362 ) ) ;
#7607=PLANE ( 'NONE',  #6002 ) ;
#7608=LINE ( 'NONE', #233, #5573 ) ;
#7611=ORIENTED_EDGE ( 'NONE', *, *, #2727, .F. ) ;
#7616=DIRECTION ( 'NONE',  ( 0.000000000000000000, -0.000000000000000000, -1.000000000000000000 ) ) ;
#7617=CARTESIAN_POINT ( 'NONE',  ( 52.50000000000000711, 111.9999999999998863, 130.0000000000000000 ) ) ;
#7619=CIRCLE ( 'NONE', #7120, 5.000000000000000888 ) ;
#7626=VECTOR ( 'NONE', #4959, 1000.000000000000000 ) ;
#7628=DIRECTION ( 'NONE',  ( 0.000000000000000000, 0.000000000000000000, -1.000000000000000000 ) ) ;
#7629=AXIS2_PLACEMENT_3D ( 'NONE', #6607, #3596, #6679 ) ;
#7634=DIRECTION ( 'NONE',  ( -1.000000000000000000, 1.387778780781445676E-15, 0.000000000000000000 ) ) ;
#7636=ORIENTED_EDGE ( 'NONE', *, *, #5475, .F. ) ;
#7638=ORIENTED_EDGE ( 'NONE', *, *, #3815, .T. ) ;
#7639=EDGE_CURVE ( 'NONE', #3593, #4754, #1038, .T. ) ;
#7640=PLANE ( 'NONE',  #3604 ) ;
#7644=CARTESIAN_POINT ( 'NONE',  ( 41.66645320948619258, 47.44875693908029035, 12.50000000000000000 ) ) ;
#7646=CARTESIAN_POINT ( 'NONE',  ( 412.4999999999998295, 150.0000000000000284, 12.50000000000000000 ) ) ;
#7647=CIRCLE ( 'NONE', #6123, 4.999999999999997335 ) ;
#7651=DIRECTION ( 'NONE',  ( 1.000000000000000000, 0.000000000000000000, 0.000000000000000000 ) ) ;
#7652=ORIENTED_EDGE ( 'NONE', *, *, #3416, .T. ) ;
#7655=DIRECTION ( 'NONE',  ( -0.000000000000000000, -0.000000000000000000, -1.000000000000000000 ) ) ;
#7656=LINE ( 'NONE', #6618, #2292 ) ;
#7658=CARTESIAN_POINT ( 'NONE',  ( 187.4999999999998863, 225.0000000000000284, 0.000000000000000000 ) ) ;
#7659=ADVANCED_FACE ( 'NONE', ( #4158 ), #7848, .T. ) ;
#7664=CARTESIAN_POINT ( 'NONE',  ( -37.49999999999989342, 187.4999999999999432, 12.50000000000000000 ) ) ;
#7665=DIRECTION ( 'NONE',  ( -0.000000000000000000, 0.000000000000000000, 1.000000000000000000 ) ) ;
#7666=CARTESIAN_POINT ( 'NONE',  ( 212.4999999999999147, 225.0000000000000284, 0.000000000000000000 ) ) ;
#7668=ADVANCED_FACE ( 'NONE', ( #1755 ), #1114, .T. ) ;
#7670=CARTESIAN_POINT ( 'NONE',  ( 47.50000000000000711, 47.50000000000003553, 5.000000000000000000 ) ) ;
#7677=LINE ( 'NONE', #4582, #6515 ) ;
#7679=EDGE_CURVE ( 'NONE', #2637, #2101, #6656, .T. ) ;
#7687=CARTESIAN_POINT ( 'NONE',  ( 326.6025403784437913, 75.00000000000005684, 125.0000000000000000 ) ) ;
#7691=CARTESIAN_POINT ( 'NONE',  ( 46.25000000000002842, 177.5000000000000000, 17.50000000000001421 ) ) ;
#7696=DIRECTION ( 'NONE',  ( -0.000000000000000000, 0.000000000000000000, 1.000000000000000000 ) ) ;
#7697=ORIENTED_EDGE ( 'NONE', *, *, #2979, .T. ) ;
#7698=CARTESIAN_POINT ( 'NONE',  ( 0.000000000000000000, 111.9999999999999858, 130.0000000000000000 ) ) ;
#7701=CARTESIAN_POINT ( 'NONE',  ( 52.50000000000000711, 177.5000000000000000, 5.000000000000000000 ) ) ;
#7702=EDGE_CURVE ( 'NONE', #511, #6088, #5489, .T. ) ;
#7703=ORIENTED_EDGE ( 'NONE', *, *, #6355, .F. ) ;
#7709=DIRECTION ( 'NONE',  ( -0.000000000000000000, -0.000000000000000000, -1.000000000000000000 ) ) ;
#7713=ORIENTED_EDGE ( 'NONE', *, *, #5807, .F. ) ;
#7717=DIRECTION ( 'NONE',  ( -4.789677997474686366E-16, -1.000000000000000000, -0.000000000000000000 ) ) ;
#7721=EDGE_CURVE ( 'NONE', #7515, #5649, #5403, .T. ) ;
#7723=ORIENTED_EDGE ( 'NONE', *, *, #4245, .T. ) ;
#7724=FACE_OUTER_BOUND ( 'NONE', #4825, .T. ) ;
#7726=EDGE_CURVE ( 'NONE', #2838, #5244, #3201, .T. ) ;
#7727=ORIENTED_EDGE ( 'NONE', *, *, #3323, .F. ) ;
#7729=ADVANCED_FACE ( 'NONE', ( #7814 ), #6654, .F. ) ;
#7730=EDGE_CURVE ( 'NONE', #2977, #1036, #2891, .T. ) ;
#7734=ORIENTED_EDGE ( 'NONE', *, *, #1795, .F. ) ;
#7737=ORIENTED_EDGE ( 'NONE', *, *, #1037, .T. ) ;
#7744=VECTOR ( 'NONE', #2707, 1000.000000000000000 ) ;
#7749=CIRCLE ( 'NONE', #4151, 5.000000000000000888 ) ;
#7753=LINE ( 'NONE', #7828, #3659 ) ;
#7760=DIRECTION ( 'NONE',  ( -1.000000000000000000, -0.000000000000000000, -0.000000000000000000 ) ) ;
#7763=DIRECTION ( 'NONE',  ( 1.000000000000000000, 0.000000000000000000, 0.000000000000000000 ) ) ;
#7764=ORIENTED_EDGE ( 'NONE', *, *, #1065, .T. ) ;
#7768=ORIENTED_EDGE ( 'NONE', *, *, #3470, .T. ) ;
#7769=DIRECTION ( 'NONE',  ( -0.000000000000000000, 1.000000000000000000, -0.000000000000000000 ) ) ;
#7778=VECTOR ( 'NONE', #3429, 1000.000000000000000 ) ;
#7779=DIRECTION ( 'NONE',  ( 0.000000000000000000, 0.000000000000000000, 1.000000000000000000 ) ) ;
#7780=VERTEX_POINT ( 'NONE', #5609 ) ;
#7781=CARTESIAN_POINT ( 'NONE',  ( 52.50000000000000711, 144.7499999999999147, 130.0000000000000000 ) ) ;
#7793=CARTESIAN_POINT ( 'NONE',  ( -37.49999999999995026, 37.50000000000010658, 12.50000000000000000 ) ) ;
#7796=PLANE ( 'NONE',  #3944 ) ;
#7800=LINE ( 'NONE', #5954, #5366 ) ;
#7804=ORIENTED_EDGE ( 'NONE', *, *, #5576, .T. ) ;
#7805=EDGE_CURVE ( 'NONE', #3051, #1999, #7005, .T. ) ;
#7806=CIRCLE ( 'NONE', #5497, 65.50000000000000000 ) ;
#7807=AXIS2_PLACEMENT_3D ( 'NONE', #1170, #3777, #6666 ) ;
#7814=FACE_OUTER_BOUND ( 'NONE', #367, .T. ) ;
#7819=CARTESIAN_POINT ( 'NONE',  ( 296.6025403784439050, 87.50000000000005684, 12.50000000000000000 ) ) ;
#7821=EDGE_CURVE ( 'NONE', #7538, #6519, #4857, .T. ) ;
#7822=DIRECTION ( 'NONE',  ( 0.000000000000000000, 1.000000000000000000, 0.000000000000000000 ) ) ;
#7824=ORIENTED_EDGE ( 'NONE', *, *, #1027, .F. ) ;
#7828=CARTESIAN_POINT ( 'NONE',  ( 286.6025403784437913, 0.000000000000000000, 0.000000000000000000 ) ) ;
#7836=LINE ( 'NONE', #3475, #5092 ) ;
#7837=CARTESIAN_POINT ( 'NONE',  ( -26.66645320948613573, 47.44875693908033298, 12.50000000000000000 ) ) ;
#7842=VERTEX_POINT ( 'NONE', #5072 ) ;
#7843=ADVANCED_FACE ( 'NONE', ( #2636, #2756 ), #7640, .F. ) ;
#7847=ORIENTED_EDGE ( 'NONE', *, *, #7394, .F. ) ;
#7848=CYLINDRICAL_SURFACE ( 'NONE', #512, 65.50000000000000000 ) ;
#7851=ORIENTED_EDGE ( 'NONE', *, *, #3554, .F. ) ;
#7852=FACE_BOUND ( 'NONE', #5070, .T. ) ;
#7853=DIRECTION ( 'NONE',  ( -0.000000000000000000, -0.000000000000000000, -1.000000000000000000 ) ) ;
#7854=ORIENTED_EDGE ( 'NONE', *, *, #7582, .F. ) ;
#7857=CARTESIAN_POINT ( 'NONE',  ( 0.000000000000000000, 0.000000000000000000, 12.50000000000000000 ) ) ;
#7860=DIRECTION ( 'NONE',  ( -0.000000000000000000, -0.000000000000000000, -1.000000000000000000 ) ) ;
#7863=DIRECTION ( 'NONE',  ( 1.000000000000000000, 0.000000000000000000, 0.000000000000000000 ) ) ;
#7874=ORIENTED_EDGE ( 'NONE', *, *, #6012, .F. ) ;
#7876=SHAPE_REPRESENTATION_RELATIONSHIP ( 'NONE' , 'NONE' ,  #444, #7563 ) ;
#7879=FACE_OUTER_BOUND ( 'NONE', #5136, .T. ) ;
#7886=CARTESIAN_POINT ( 'NONE',  ( 296.6025403784439050, 142.5000000000000000, 125.0000000000000000 ) ) ;
#7892=CARTESIAN_POINT ( 'NONE',  ( -27.49999999999994671, 37.50000000000008527, 12.50000000000000000 ) ) ;
#7893=EDGE_CURVE ( 'NONE', #7188, #7382, #1928, .T. ) ;
#7900=CARTESIAN_POINT ( 'NONE',  ( -37.49999999999994316, 225.0000000000000284, 12.50000000000000000 ) ) ;
#7902=DIRECTION ( 'NONE',  ( 0.000000000000000000, 1.000000000000000000, 0.000000000000000000 ) ) ;
#7906=PRODUCT_DEFINITION ( 'UNKNOWN', '', #6171, #2960 ) ;
#7907=DIRECTION ( 'NONE',  ( -1.000000000000000000, 0.000000000000000000, 0.000000000000000000 ) ) ;
#7909=DIRECTION ( 'NONE',  ( 0.000000000000000000, -0.000000000000000000, -1.000000000000000000 ) ) ;
#7910=AXIS2_PLACEMENT_3D ( 'NONE', #3494, #2935, #6576 ) ;
#7911=CIRCLE ( 'NONE', #2795, 37.50000000000000711 ) ;
#7914=AXIS2_PLACEMENT_3D ( 'NONE', #1632, #2885, #4596 ) ;
#7916=ORIENTED_EDGE ( 'NONE', *, *, #168, .F. ) ;
#7935=COLOUR_RGB('Dark Blue',0.08,0.2,0.34);
#7936=FILL_AREA_STYLE_COLOUR('',#7935);
#7937=FILL_AREA_STYLE('',(#7936));
#7938=SURFACE_STYLE_FILL_AREA(#7937);
#7939=SURFACE_SIDE_STYLE('',(#7938));
#7940=SURFACE_STYLE_USAGE(.BOTH.,#7939);
#7941=PRESENTATION_STYLE_ASSIGNMENT((#7940));
ENDSEC;
END-ISO-10303-21;
